ISO-10303-21;
HEADER;
/* Generated by software containing ST-Developer
 * from STEP Tools, Inc. (www.steptools.com) 
 */
/* OPTION: using custom renumber hook */

FILE_DESCRIPTION(
/* description */ ('STEP AP242 Edition 2', 'CAx-IF Rec.Pracs.---Representation and Presentation of Product Manufa
cturing Information (PMI)---4.0---2014-10-13', 'CAx-IF Rec.Pracs.---3D Tessellated Geometry---0.4---2014-09-14', '2;1', 'CAx-IF Rec.Pracs.---User Defined Attributes---1.5---2016-08-15'),
/* implementation_level */ '2;1');

FILE_NAME(
/* name */ 'refill_port__PD45609.step',
/* time_stamp */ '2026-10-08T12:15:07Z',
/* author */ (''),
/* organization */ (''),
/* preprocessor_version */ 'ST-DEVELOPER v20',
/* originating_system */ 'ONSHAPE BY PTC INC, 1.221',
/* authorisation */ '  ');

FILE_SCHEMA (('AP242_MANAGED_MODEL_BASED_3D_ENGINEERING_MIM_LF { 1 0 10303 442 3 1 4 }'));
ENDSEC;

DATA;
#31=CONICAL_SURFACE('',#15183,0.001,0.34906585039887);
#60=COLOUR_RGB('', 0.66274510, 0.83137255, 0.94901961);
#224=SHAPE_REPRESENTATION_RELATIONSHIP('','',#13798,#251);
#251=ADVANCED_BREP_SHAPE_REPRESENTATION('',(#13742),#45488);
#976=CIRCLE('',#15129,0.00227296943362564);
#977=CIRCLE('',#15130,0.000477030566374308);
#978=CIRCLE('',#15131,0.00322703056637426);
#979=CIRCLE('',#15132,0.000477030566374308);
#980=CIRCLE('',#15134,0.00322703056637426);
#981=CIRCLE('',#15136,0.00227296943362564);
#982=CIRCLE('',#15138,0.000477030566374308);
#983=CIRCLE('',#15139,0.00227296943362574);
#984=CIRCLE('',#15140,0.000477030566374308);
#985=CIRCLE('',#15141,0.00322703056637436);
#986=CIRCLE('',#15143,0.000477030566374308);
#987=CIRCLE('',#15145,0.000477030566374308);
#988=CIRCLE('',#15147,0.008);
#989=CIRCLE('',#15148,0.0035);
#990=CIRCLE('',#15149,0.008);
#991=CIRCLE('',#15150,0.0025);
#992=CIRCLE('',#15155,0.00209191070279862);
#993=CIRCLE('',#15156,0.00209191070279862);
#994=CIRCLE('',#15158,0.0015);
#995=CIRCLE('',#15159,0.001);
#996=CIRCLE('',#15161,0.008);
#997=CIRCLE('',#15162,0.008);
#998=CIRCLE('',#15164,0.0015);
#999=CIRCLE('',#15165,0.0099);
#1000=CIRCLE('',#15166,0.0025);
#1001=CIRCLE('',#15171,0.000477030566374308);
#1002=CIRCLE('',#15172,0.000477030566374308);
#1003=CIRCLE('',#15173,0.008);
#1004=CIRCLE('',#15174,0.0099);
#1005=CIRCLE('',#15175,0.0035);
#1006=CIRCLE('',#15176,0.00322703056637436);
#1007=CIRCLE('',#15177,0.00227296943362574);
#1008=CIRCLE('',#15182,0.001);
#1148=B_SPLINE_CURVE_WITH_KNOTS('',3,(#41775,#41776,#41777,#41778,#41779),
 .UNSPECIFIED.,.F.,.F.,(4,1,4),(-0.000755554523882612,6.89428958346064E-7,
0.000756933381799304),.UNSPECIFIED.);
#1513=PLANE('',#15128);
#1514=PLANE('',#15137);
#1515=PLANE('',#15146);
#1516=PLANE('',#15152);
#1517=PLANE('',#15153);
#1518=PLANE('',#15157);
#1519=PLANE('',#15163);
#1520=PLANE('',#15167);
#1521=PLANE('',#15168);
#1522=PLANE('',#15170);
#1792=CYLINDRICAL_SURFACE('',#15133,0.00322703056637436);
#1793=CYLINDRICAL_SURFACE('',#15135,0.00227296943362574);
#1794=CYLINDRICAL_SURFACE('',#15142,0.000477030566374308);
#1795=CYLINDRICAL_SURFACE('',#15144,0.000477030566374308);
#1796=CYLINDRICAL_SURFACE('',#15151,0.0107118988125);
#1797=CYLINDRICAL_SURFACE('',#15154,0.00209191070279862);
#1798=CYLINDRICAL_SURFACE('',#15160,0.008);
#1799=CYLINDRICAL_SURFACE('',#15169,0.0025);
#1800=CYLINDRICAL_SURFACE('',#15178,0.0099);
#1801=CYLINDRICAL_SURFACE('',#15179,0.008);
#1802=CYLINDRICAL_SURFACE('',#15180,0.0015);
#1803=CYLINDRICAL_SURFACE('',#15181,0.001);
#1804=CYLINDRICAL_SURFACE('',#15184,0.0035);
#1805=CYLINDRICAL_SURFACE('',#15185,0.00322703056637436);
#1806=CYLINDRICAL_SURFACE('',#15186,0.00227296943362574);
#1807=CYLINDRICAL_SURFACE('',#15187,0.000477030566374308);
#1808=CYLINDRICAL_SURFACE('',#15188,0.000477030566374308);
#1948=(
BOUNDED_CURVE()
B_SPLINE_CURVE(2,(#41291,#41292,#41293,#41294,#41295,#41296,#41297,#41298,
#41299,#41300,#41301,#41302,#41303,#41304,#41305,#41306,#41307,#41308,#41309,
#41310,#41311,#41312,#41313,#41314,#41315,#41316,#41317,#41318,#41319,#41320,
#41321,#41322,#41323,#41324,#41325,#41326,#41327,#41328,#41329,#41330,#41331,
#41332,#41333,#41334,#41335,#41336,#41337,#41338,#41339,#41340,#41341,#41342,
#41343,#41344,#41345,#41346,#41347,#41348,#41349,#41350,#41351,#41352,#41353,
#41354,#41355),.UNSPECIFIED.,.F.,.F.)
B_SPLINE_CURVE_WITH_KNOTS((3,2,2,2,2,2,2,2,2,2,2,2,2,2,2,2,2,2,2,2,2,2,
2,2,2,2,2,2,2,2,2,2,3),(0.,0.03125,0.0625,0.09375,0.125,0.15625,0.1875,
0.21875,0.25,0.28125,0.3125,0.34375,0.375,0.40625,0.4375,0.46875,0.5,0.53125,
0.5625,0.59375,0.625,0.65625,0.6875,0.71875,0.75,0.78125,0.8125,0.84375,
0.875,0.90625,0.9375,0.96875,1.),.UNSPECIFIED.)
CURVE()
GEOMETRIC_REPRESENTATION_ITEM()
RATIONAL_B_SPLINE_CURVE((1.,0.923879532511287,1.,0.923879532511287,1.,0.923879532511287,
1.,0.923879532511287,1.,0.923879532511287,1.,0.923879532511287,1.,0.923879532511287,
1.,0.923879532511287,1.,0.923879532511287,1.,0.923879532511287,1.,0.923879532511287,
1.,0.923879532511287,1.,0.923879532511287,1.,0.923879532511287,1.,0.923879532511287,
1.,0.923879532511287,1.,0.923879532511287,1.,0.923879532511287,1.,0.923879532511287,
1.,0.923879532511287,1.,0.923879532511287,1.,0.923879532511287,1.,0.923879532511287,
1.,0.923879532511287,1.,0.923879532511287,1.,0.923879532511287,1.,0.923879532511287,
1.,0.923879532511287,1.,0.923879532511287,1.,0.923879532511287,1.,0.923879532511287,
1.,0.923879532511287,1.))
REPRESENTATION_ITEM('')
);
#1949=(
BOUNDED_CURVE()
B_SPLINE_CURVE(2,(#41359,#41360,#41361,#41362,#41363,#41364,#41365,#41366,
#41367),.UNSPECIFIED.,.F.,.F.)
B_SPLINE_CURVE_WITH_KNOTS((3,2,2,2,3),(0.875,0.90625,0.9375,0.96875,1.),
 .UNSPECIFIED.)
CURVE()
GEOMETRIC_REPRESENTATION_ITEM()
RATIONAL_B_SPLINE_CURVE((1.,0.923879532511287,1.,0.923879532511287,1.,0.923879532511287,
1.,0.923879532511287,1.))
REPRESENTATION_ITEM('')
);
#1950=(
BOUNDED_CURVE()
B_SPLINE_CURVE(2,(#41369,#41370,#41371,#41372,#41373,#41374,#41375,#41376,
#41377),.UNSPECIFIED.,.F.,.F.)
B_SPLINE_CURVE_WITH_KNOTS((3,2,2,2,3),(0.75,0.78125,0.8125,0.84375,0.875),
 .UNSPECIFIED.)
CURVE()
GEOMETRIC_REPRESENTATION_ITEM()
RATIONAL_B_SPLINE_CURVE((1.,0.923879532511287,1.,0.923879532511287,1.,0.923879532511287,
1.,0.923879532511287,1.))
REPRESENTATION_ITEM('')
);
#1951=(
BOUNDED_CURVE()
B_SPLINE_CURVE(2,(#41379,#41380,#41381,#41382,#41383,#41384,#41385,#41386,
#41387),.UNSPECIFIED.,.F.,.F.)
B_SPLINE_CURVE_WITH_KNOTS((3,2,2,2,3),(0.625,0.65625,0.6875,0.71875,0.75),
 .UNSPECIFIED.)
CURVE()
GEOMETRIC_REPRESENTATION_ITEM()
RATIONAL_B_SPLINE_CURVE((1.,0.923879532511287,1.,0.923879532511287,1.,0.923879532511287,
1.,0.923879532511287,1.))
REPRESENTATION_ITEM('')
);
#1952=(
BOUNDED_CURVE()
B_SPLINE_CURVE(2,(#41389,#41390,#41391,#41392,#41393,#41394,#41395,#41396,
#41397),.UNSPECIFIED.,.F.,.F.)
B_SPLINE_CURVE_WITH_KNOTS((3,2,2,2,3),(0.5,0.53125,0.5625,0.59375,0.625),
 .UNSPECIFIED.)
CURVE()
GEOMETRIC_REPRESENTATION_ITEM()
RATIONAL_B_SPLINE_CURVE((1.,0.923879532511286,1.,0.923879532511287,1.,0.923879532511287,
1.,0.923879532511287,1.))
REPRESENTATION_ITEM('')
);
#1953=(
BOUNDED_CURVE()
B_SPLINE_CURVE(2,(#41399,#41400,#41401,#41402,#41403,#41404,#41405,#41406,
#41407),.UNSPECIFIED.,.F.,.F.)
B_SPLINE_CURVE_WITH_KNOTS((3,2,2,2,3),(0.375,0.40625,0.4375,0.46875,0.5),
 .UNSPECIFIED.)
CURVE()
GEOMETRIC_REPRESENTATION_ITEM()
RATIONAL_B_SPLINE_CURVE((1.,0.923879532511286,1.,0.923879532511287,1.,0.923879532511287,
1.,0.923879532511287,1.))
REPRESENTATION_ITEM('')
);
#1954=(
BOUNDED_CURVE()
B_SPLINE_CURVE(2,(#41409,#41410,#41411,#41412,#41413,#41414,#41415,#41416,
#41417),.UNSPECIFIED.,.F.,.F.)
B_SPLINE_CURVE_WITH_KNOTS((3,2,2,2,3),(0.25,0.28125,0.3125,0.34375,0.375),
 .UNSPECIFIED.)
CURVE()
GEOMETRIC_REPRESENTATION_ITEM()
RATIONAL_B_SPLINE_CURVE((1.,0.923879532511287,1.,0.923879532511287,1.,0.923879532511287,
1.,0.923879532511288,1.))
REPRESENTATION_ITEM('')
);
#1955=(
BOUNDED_CURVE()
B_SPLINE_CURVE(2,(#41419,#41420,#41421,#41422,#41423,#41424,#41425,#41426,
#41427),.UNSPECIFIED.,.F.,.F.)
B_SPLINE_CURVE_WITH_KNOTS((3,2,2,2,3),(0.125,0.15625,0.1875,0.21875,0.25),
 .UNSPECIFIED.)
CURVE()
GEOMETRIC_REPRESENTATION_ITEM()
RATIONAL_B_SPLINE_CURVE((1.,0.923879532511287,1.,0.923879532511287,1.,0.923879532511287,
1.,0.923879532511286,1.))
REPRESENTATION_ITEM('')
);
#1956=(
BOUNDED_CURVE()
B_SPLINE_CURVE(2,(#41429,#41430,#41431,#41432,#41433,#41434,#41435,#41436,
#41437),.UNSPECIFIED.,.F.,.F.)
B_SPLINE_CURVE_WITH_KNOTS((3,2,2,2,3),(0.,0.03125,0.0625,0.09375,0.125),
 .UNSPECIFIED.)
CURVE()
GEOMETRIC_REPRESENTATION_ITEM()
RATIONAL_B_SPLINE_CURVE((1.,0.923879532511287,1.,0.923879532511287,1.,0.923879532511287,
1.,0.923879532511287,1.))
REPRESENTATION_ITEM('')
);
#1957=(
BOUNDED_CURVE()
B_SPLINE_CURVE(2,(#41571,#41572,#41573,#41574,#41575,#41576,#41577,#41578,
#41579),.UNSPECIFIED.,.F.,.F.)
B_SPLINE_CURVE_WITH_KNOTS((3,2,2,2,3),(0.,0.03125,0.0625,0.09375,0.125),
 .UNSPECIFIED.)
CURVE()
GEOMETRIC_REPRESENTATION_ITEM()
RATIONAL_B_SPLINE_CURVE((1.,0.923879532511287,1.,0.923879532511287,1.,0.923879532511287,
1.,0.923879532511287,1.))
REPRESENTATION_ITEM('')
);
#1958=(
BOUNDED_CURVE()
B_SPLINE_CURVE(2,(#41581,#41582,#41583,#41584,#41585,#41586,#41587,#41588,
#41589),.UNSPECIFIED.,.F.,.F.)
B_SPLINE_CURVE_WITH_KNOTS((3,2,2,2,3),(0.125,0.15625,0.1875,0.21875,0.25),
 .UNSPECIFIED.)
CURVE()
GEOMETRIC_REPRESENTATION_ITEM()
RATIONAL_B_SPLINE_CURVE((1.,0.923879532511287,1.,0.923879532511287,1.,0.923879532511287,
1.,0.923879532511286,1.))
REPRESENTATION_ITEM('')
);
#1959=(
BOUNDED_CURVE()
B_SPLINE_CURVE(2,(#41591,#41592,#41593,#41594,#41595,#41596,#41597,#41598,
#41599),.UNSPECIFIED.,.F.,.F.)
B_SPLINE_CURVE_WITH_KNOTS((3,2,2,2,3),(0.25,0.28125,0.3125,0.34375,0.375),
 .UNSPECIFIED.)
CURVE()
GEOMETRIC_REPRESENTATION_ITEM()
RATIONAL_B_SPLINE_CURVE((1.,0.923879532511287,1.,0.923879532511287,1.,0.923879532511287,
1.,0.923879532511286,1.))
REPRESENTATION_ITEM('')
);
#1960=(
BOUNDED_CURVE()
B_SPLINE_CURVE(2,(#41601,#41602,#41603,#41604,#41605,#41606,#41607,#41608,
#41609),.UNSPECIFIED.,.F.,.F.)
B_SPLINE_CURVE_WITH_KNOTS((3,2,2,2,3),(0.375,0.40625,0.4375,0.46875,0.5),
 .UNSPECIFIED.)
CURVE()
GEOMETRIC_REPRESENTATION_ITEM()
RATIONAL_B_SPLINE_CURVE((1.,0.923879532511287,1.,0.923879532511287,1.,0.923879532511287,
1.,0.923879532511287,1.))
REPRESENTATION_ITEM('')
);
#1961=(
BOUNDED_CURVE()
B_SPLINE_CURVE(2,(#41611,#41612,#41613,#41614,#41615,#41616,#41617,#41618,
#41619),.UNSPECIFIED.,.F.,.F.)
B_SPLINE_CURVE_WITH_KNOTS((3,2,2,2,3),(0.5,0.53125,0.5625,0.59375,0.625),
 .UNSPECIFIED.)
CURVE()
GEOMETRIC_REPRESENTATION_ITEM()
RATIONAL_B_SPLINE_CURVE((1.,0.923879532511286,1.,0.923879532511287,1.,0.923879532511287,
1.,0.923879532511287,1.))
REPRESENTATION_ITEM('')
);
#1962=(
BOUNDED_CURVE()
B_SPLINE_CURVE(2,(#41621,#41622,#41623,#41624,#41625,#41626,#41627,#41628,
#41629),.UNSPECIFIED.,.F.,.F.)
B_SPLINE_CURVE_WITH_KNOTS((3,2,2,2,3),(0.625,0.65625,0.6875,0.71875,0.75),
 .UNSPECIFIED.)
CURVE()
GEOMETRIC_REPRESENTATION_ITEM()
RATIONAL_B_SPLINE_CURVE((1.,0.923879532511287,1.,0.923879532511287,1.,0.923879532511287,
1.,0.923879532511287,1.))
REPRESENTATION_ITEM('')
);
#1963=(
BOUNDED_CURVE()
B_SPLINE_CURVE(2,(#41631,#41632,#41633,#41634,#41635,#41636,#41637,#41638,
#41639),.UNSPECIFIED.,.F.,.F.)
B_SPLINE_CURVE_WITH_KNOTS((3,2,2,2,3),(0.75,0.78125,0.8125,0.84375,0.875),
 .UNSPECIFIED.)
CURVE()
GEOMETRIC_REPRESENTATION_ITEM()
RATIONAL_B_SPLINE_CURVE((1.,0.923879532511287,1.,0.923879532511287,1.,0.923879532511287,
1.,0.923879532511287,1.))
REPRESENTATION_ITEM('')
);
#1964=(
BOUNDED_CURVE()
B_SPLINE_CURVE(2,(#41641,#41642,#41643,#41644,#41645,#41646,#41647,#41648,
#41649),.UNSPECIFIED.,.F.,.F.)
B_SPLINE_CURVE_WITH_KNOTS((3,2,2,2,3),(0.875,0.90625,0.9375,0.96875,1.),
 .UNSPECIFIED.)
CURVE()
GEOMETRIC_REPRESENTATION_ITEM()
RATIONAL_B_SPLINE_CURVE((1.,0.923879532511287,1.,0.923879532511287,1.,0.923879532511287,
1.,0.923879532511287,1.))
REPRESENTATION_ITEM('')
);
#1965=(
BOUNDED_CURVE()
B_SPLINE_CURVE(2,(#41653,#41654,#41655,#41656,#41657,#41658,#41659,#41660,
#41661,#41662,#41663,#41664,#41665,#41666,#41667,#41668,#41669,#41670,#41671,
#41672,#41673,#41674,#41675,#41676,#41677,#41678,#41679,#41680,#41681,#41682,
#41683,#41684,#41685,#41686,#41687,#41688,#41689,#41690,#41691,#41692,#41693,
#41694,#41695,#41696,#41697,#41698,#41699,#41700,#41701,#41702,#41703,#41704,
#41705,#41706,#41707,#41708,#41709,#41710,#41711,#41712,#41713,#41714,#41715,
#41716,#41717),.UNSPECIFIED.,.F.,.F.)
B_SPLINE_CURVE_WITH_KNOTS((3,2,2,2,2,2,2,2,2,2,2,2,2,2,2,2,2,2,2,2,2,2,
2,2,2,2,2,2,2,2,2,2,3),(0.,0.03125,0.0625,0.09375,0.125,0.15625,0.1875,
0.21875,0.25,0.28125,0.3125,0.34375,0.375,0.40625,0.4375,0.46875,0.5,0.53125,
0.5625,0.59375,0.625,0.65625,0.6875,0.71875,0.75,0.78125,0.8125,0.84375,
0.875,0.90625,0.9375,0.96875,1.),.UNSPECIFIED.)
CURVE()
GEOMETRIC_REPRESENTATION_ITEM()
RATIONAL_B_SPLINE_CURVE((1.,0.923879532511287,1.,0.923879532511287,1.,0.923879532511287,
1.,0.923879532511287,1.,0.923879532511287,1.,0.923879532511287,1.,0.923879532511287,
1.,0.923879532511287,1.,0.923879532511287,1.,0.923879532511287,1.,0.923879532511287,
1.,0.923879532511287,1.,0.923879532511287,1.,0.923879532511287,1.,0.923879532511287,
1.,0.923879532511287,1.,0.923879532511287,1.,0.923879532511287,1.,0.923879532511287,
1.,0.923879532511287,1.,0.923879532511287,1.,0.923879532511287,1.,0.923879532511287,
1.,0.923879532511287,1.,0.923879532511287,1.,0.923879532511287,1.,0.923879532511287,
1.,0.923879532511287,1.,0.923879532511287,1.,0.923879532511287,1.,0.923879532511287,
1.,0.923879532511287,1.))
REPRESENTATION_ITEM('')
);
#5180=ORIENTED_EDGE('',*,*,#7237,.T.);
#5181=ORIENTED_EDGE('',*,*,#7238,.T.);
#5182=ORIENTED_EDGE('',*,*,#7239,.T.);
#5183=ORIENTED_EDGE('',*,*,#7240,.T.);
#5184=ORIENTED_EDGE('',*,*,#7241,.T.);
#5185=ORIENTED_EDGE('',*,*,#7242,.F.);
#5186=ORIENTED_EDGE('',*,*,#7239,.F.);
#5187=ORIENTED_EDGE('',*,*,#7243,.T.);
#5188=ORIENTED_EDGE('',*,*,#7244,.T.);
#5189=ORIENTED_EDGE('',*,*,#7245,.F.);
#5190=ORIENTED_EDGE('',*,*,#7237,.F.);
#5191=ORIENTED_EDGE('',*,*,#7246,.T.);
#5192=ORIENTED_EDGE('',*,*,#7247,.T.);
#5193=ORIENTED_EDGE('',*,*,#7248,.T.);
#5194=ORIENTED_EDGE('',*,*,#7249,.T.);
#5195=ORIENTED_EDGE('',*,*,#7250,.T.);
#5196=ORIENTED_EDGE('',*,*,#7251,.T.);
#5197=ORIENTED_EDGE('',*,*,#7252,.F.);
#5198=ORIENTED_EDGE('',*,*,#7249,.F.);
#5199=ORIENTED_EDGE('',*,*,#7253,.T.);
#5200=ORIENTED_EDGE('',*,*,#7254,.T.);
#5201=ORIENTED_EDGE('',*,*,#7255,.F.);
#5202=ORIENTED_EDGE('',*,*,#7247,.F.);
#5203=ORIENTED_EDGE('',*,*,#7256,.T.);
#5204=ORIENTED_EDGE('',*,*,#7257,.F.);
#5205=ORIENTED_EDGE('',*,*,#7258,.T.);
#5206=ORIENTED_EDGE('',*,*,#7259,.F.);
#5207=ORIENTED_EDGE('',*,*,#7260,.T.);
#5208=ORIENTED_EDGE('',*,*,#7261,.F.);
#5209=ORIENTED_EDGE('',*,*,#7262,.T.);
#5210=ORIENTED_EDGE('',*,*,#7263,.F.);
#5211=ORIENTED_EDGE('',*,*,#7264,.T.);
#5212=ORIENTED_EDGE('',*,*,#7265,.F.);
#5213=ORIENTED_EDGE('',*,*,#7266,.F.);
#5214=ORIENTED_EDGE('',*,*,#7267,.F.);
#5215=ORIENTED_EDGE('',*,*,#7268,.F.);
#5216=ORIENTED_EDGE('',*,*,#7269,.F.);
#5217=ORIENTED_EDGE('',*,*,#7270,.F.);
#5218=ORIENTED_EDGE('',*,*,#7271,.F.);
#5219=ORIENTED_EDGE('',*,*,#7272,.F.);
#5220=ORIENTED_EDGE('',*,*,#7273,.F.);
#5221=ORIENTED_EDGE('',*,*,#7274,.F.);
#5222=ORIENTED_EDGE('',*,*,#7275,.T.);
#5223=ORIENTED_EDGE('',*,*,#7276,.T.);
#5224=ORIENTED_EDGE('',*,*,#7277,.T.);
#5225=ORIENTED_EDGE('',*,*,#7278,.T.);
#5226=ORIENTED_EDGE('',*,*,#7279,.T.);
#5227=ORIENTED_EDGE('',*,*,#7280,.T.);
#5228=ORIENTED_EDGE('',*,*,#7281,.T.);
#5229=ORIENTED_EDGE('',*,*,#7282,.T.);
#5230=ORIENTED_EDGE('',*,*,#7283,.F.);
#5231=ORIENTED_EDGE('',*,*,#7284,.F.);
#5232=ORIENTED_EDGE('',*,*,#7285,.F.);
#5233=ORIENTED_EDGE('',*,*,#7284,.T.);
#5234=ORIENTED_EDGE('',*,*,#7286,.F.);
#5235=ORIENTED_EDGE('',*,*,#7264,.F.);
#5236=ORIENTED_EDGE('',*,*,#7286,.T.);
#5237=ORIENTED_EDGE('',*,*,#7283,.T.);
#5238=ORIENTED_EDGE('',*,*,#7287,.T.);
#5239=ORIENTED_EDGE('',*,*,#7265,.T.);
#5240=ORIENTED_EDGE('',*,*,#7285,.T.);
#5241=ORIENTED_EDGE('',*,*,#7263,.T.);
#5242=ORIENTED_EDGE('',*,*,#7288,.T.);
#5243=ORIENTED_EDGE('',*,*,#7274,.T.);
#5244=ORIENTED_EDGE('',*,*,#7289,.T.);
#5245=ORIENTED_EDGE('',*,*,#7290,.T.);
#5246=ORIENTED_EDGE('',*,*,#7291,.T.);
#5247=ORIENTED_EDGE('',*,*,#7292,.T.);
#5248=ORIENTED_EDGE('',*,*,#7293,.T.);
#5249=ORIENTED_EDGE('',*,*,#7294,.F.);
#5250=ORIENTED_EDGE('',*,*,#7260,.F.);
#5251=ORIENTED_EDGE('',*,*,#7295,.T.);
#5252=ORIENTED_EDGE('',*,*,#7296,.T.);
#5253=ORIENTED_EDGE('',*,*,#7297,.T.);
#5254=ORIENTED_EDGE('',*,*,#7258,.F.);
#5255=ORIENTED_EDGE('',*,*,#7298,.T.);
#5256=ORIENTED_EDGE('',*,*,#7299,.T.);
#5257=ORIENTED_EDGE('',*,*,#7300,.F.);
#5258=ORIENTED_EDGE('',*,*,#7301,.F.);
#5259=ORIENTED_EDGE('',*,*,#7302,.F.);
#5260=ORIENTED_EDGE('',*,*,#7299,.F.);
#5261=ORIENTED_EDGE('',*,*,#7303,.T.);
#5262=ORIENTED_EDGE('',*,*,#7304,.T.);
#5263=ORIENTED_EDGE('',*,*,#7305,.T.);
#5264=ORIENTED_EDGE('',*,*,#7306,.F.);
#5265=ORIENTED_EDGE('',*,*,#7261,.T.);
#5266=ORIENTED_EDGE('',*,*,#7300,.T.);
#5267=ORIENTED_EDGE('',*,*,#7305,.F.);
#5268=ORIENTED_EDGE('',*,*,#7298,.F.);
#5269=ORIENTED_EDGE('',*,*,#7257,.T.);
#5270=ORIENTED_EDGE('',*,*,#7307,.T.);
#5271=ORIENTED_EDGE('',*,*,#7303,.F.);
#5272=ORIENTED_EDGE('',*,*,#7307,.F.);
#5273=ORIENTED_EDGE('',*,*,#7262,.F.);
#5274=ORIENTED_EDGE('',*,*,#7306,.T.);
#5275=ORIENTED_EDGE('',*,*,#7304,.F.);
#5276=ORIENTED_EDGE('',*,*,#7308,.F.);
#5277=ORIENTED_EDGE('',*,*,#7244,.F.);
#5278=ORIENTED_EDGE('',*,*,#7309,.F.);
#5279=ORIENTED_EDGE('',*,*,#7241,.F.);
#5280=ORIENTED_EDGE('',*,*,#7292,.F.);
#5281=ORIENTED_EDGE('',*,*,#7310,.F.);
#5282=ORIENTED_EDGE('',*,*,#7311,.T.);
#5283=ORIENTED_EDGE('',*,*,#7296,.F.);
#5284=ORIENTED_EDGE('',*,*,#7312,.T.);
#5285=ORIENTED_EDGE('',*,*,#7254,.F.);
#5286=ORIENTED_EDGE('',*,*,#7313,.F.);
#5287=ORIENTED_EDGE('',*,*,#7251,.F.);
#5288=ORIENTED_EDGE('',*,*,#7314,.F.);
#5289=ORIENTED_EDGE('',*,*,#7267,.T.);
#5290=ORIENTED_EDGE('',*,*,#7266,.T.);
#5291=ORIENTED_EDGE('',*,*,#7287,.F.);
#5292=ORIENTED_EDGE('',*,*,#7282,.F.);
#5293=ORIENTED_EDGE('',*,*,#7281,.F.);
#5294=ORIENTED_EDGE('',*,*,#7280,.F.);
#5295=ORIENTED_EDGE('',*,*,#7279,.F.);
#5296=ORIENTED_EDGE('',*,*,#7278,.F.);
#5297=ORIENTED_EDGE('',*,*,#7277,.F.);
#5298=ORIENTED_EDGE('',*,*,#7276,.F.);
#5299=ORIENTED_EDGE('',*,*,#7275,.F.);
#5300=ORIENTED_EDGE('',*,*,#7311,.F.);
#5301=ORIENTED_EDGE('',*,*,#7288,.F.);
#5302=ORIENTED_EDGE('',*,*,#7273,.T.);
#5303=ORIENTED_EDGE('',*,*,#7272,.T.);
#5304=ORIENTED_EDGE('',*,*,#7271,.T.);
#5305=ORIENTED_EDGE('',*,*,#7270,.T.);
#5306=ORIENTED_EDGE('',*,*,#7269,.T.);
#5307=ORIENTED_EDGE('',*,*,#7268,.T.);
#5308=ORIENTED_EDGE('',*,*,#7302,.T.);
#5309=ORIENTED_EDGE('',*,*,#7310,.T.);
#5310=ORIENTED_EDGE('',*,*,#7291,.F.);
#5311=ORIENTED_EDGE('',*,*,#7315,.F.);
#5312=ORIENTED_EDGE('',*,*,#7289,.F.);
#5313=ORIENTED_EDGE('',*,*,#7301,.T.);
#5314=ORIENTED_EDGE('',*,*,#7293,.F.);
#5315=ORIENTED_EDGE('',*,*,#7294,.T.);
#5316=ORIENTED_EDGE('',*,*,#7316,.F.);
#5317=ORIENTED_EDGE('',*,*,#7290,.F.);
#5318=ORIENTED_EDGE('',*,*,#7315,.T.);
#5319=ORIENTED_EDGE('',*,*,#7316,.T.);
#5320=ORIENTED_EDGE('',*,*,#7259,.T.);
#5321=ORIENTED_EDGE('',*,*,#7297,.F.);
#5322=ORIENTED_EDGE('',*,*,#7312,.F.);
#5323=ORIENTED_EDGE('',*,*,#7295,.F.);
#5324=ORIENTED_EDGE('',*,*,#7250,.F.);
#5325=ORIENTED_EDGE('',*,*,#7252,.T.);
#5326=ORIENTED_EDGE('',*,*,#7313,.T.);
#5327=ORIENTED_EDGE('',*,*,#7256,.F.);
#5328=ORIENTED_EDGE('',*,*,#7248,.F.);
#5329=ORIENTED_EDGE('',*,*,#7255,.T.);
#5330=ORIENTED_EDGE('',*,*,#7314,.T.);
#5331=ORIENTED_EDGE('',*,*,#7253,.F.);
#5332=ORIENTED_EDGE('',*,*,#7238,.F.);
#5333=ORIENTED_EDGE('',*,*,#7245,.T.);
#5334=ORIENTED_EDGE('',*,*,#7308,.T.);
#5335=ORIENTED_EDGE('',*,*,#7243,.F.);
#5336=ORIENTED_EDGE('',*,*,#7240,.F.);
#5337=ORIENTED_EDGE('',*,*,#7242,.T.);
#5338=ORIENTED_EDGE('',*,*,#7309,.T.);
#5339=ORIENTED_EDGE('',*,*,#7246,.F.);
#7237=EDGE_CURVE('',#8619,#8620,#976,.T.);
#7238=EDGE_CURVE('',#8620,#8621,#977,.T.);
#7239=EDGE_CURVE('',#8621,#8622,#978,.T.);
#7240=EDGE_CURVE('',#8622,#8619,#979,.T.);
#7241=EDGE_CURVE('',#8623,#8624,#980,.T.);
#7242=EDGE_CURVE('',#8622,#8624,#9533,.T.);
#7243=EDGE_CURVE('',#8621,#8623,#9534,.T.);
#7244=EDGE_CURVE('',#8625,#8626,#981,.T.);
#7245=EDGE_CURVE('',#8620,#8626,#9535,.T.);
#7246=EDGE_CURVE('',#8619,#8625,#9536,.T.);
#7247=EDGE_CURVE('',#8627,#8628,#982,.T.);
#7248=EDGE_CURVE('',#8628,#8629,#983,.T.);
#7249=EDGE_CURVE('',#8629,#8630,#984,.T.);
#7250=EDGE_CURVE('',#8630,#8627,#985,.T.);
#7251=EDGE_CURVE('',#8631,#8632,#986,.T.);
#7252=EDGE_CURVE('',#8630,#8632,#9537,.T.);
#7253=EDGE_CURVE('',#8629,#8631,#9538,.T.);
#7254=EDGE_CURVE('',#8633,#8634,#987,.T.);
#7255=EDGE_CURVE('',#8628,#8634,#9539,.T.);
#7256=EDGE_CURVE('',#8627,#8633,#9540,.T.);
#7257=EDGE_CURVE('',#8635,#8636,#9541,.T.);
#7258=EDGE_CURVE('',#8635,#8637,#988,.T.);
#7259=EDGE_CURVE('',#8638,#8637,#989,.T.);
#7260=EDGE_CURVE('',#8638,#8639,#990,.T.);
#7261=EDGE_CURVE('',#8640,#8639,#9542,.T.);
#7262=EDGE_CURVE('',#8640,#8636,#991,.T.);
#7263=EDGE_CURVE('',#8641,#8642,#9543,.T.);
#7264=EDGE_CURVE('',#8641,#8643,#1948,.T.);
#7265=EDGE_CURVE('',#8644,#8643,#9544,.T.);
#7266=EDGE_CURVE('',#8645,#8644,#1949,.T.);
#7267=EDGE_CURVE('',#8646,#8645,#1950,.T.);
#7268=EDGE_CURVE('',#8647,#8646,#1951,.T.);
#7269=EDGE_CURVE('',#8648,#8647,#1952,.T.);
#7270=EDGE_CURVE('',#8649,#8648,#1953,.T.);
#7271=EDGE_CURVE('',#8650,#8649,#1954,.T.);
#7272=EDGE_CURVE('',#8651,#8650,#1955,.T.);
#7273=EDGE_CURVE('',#8642,#8651,#1956,.T.);
#7274=EDGE_CURVE('',#8652,#8653,#9545,.T.);
#7275=EDGE_CURVE('',#8652,#8654,#1957,.T.);
#7276=EDGE_CURVE('',#8654,#8655,#1958,.T.);
#7277=EDGE_CURVE('',#8655,#8656,#1959,.T.);
#7278=EDGE_CURVE('',#8656,#8657,#1960,.T.);
#7279=EDGE_CURVE('',#8657,#8658,#1961,.T.);
#7280=EDGE_CURVE('',#8658,#8659,#1962,.T.);
#7281=EDGE_CURVE('',#8659,#8660,#1963,.T.);
#7282=EDGE_CURVE('',#8660,#8661,#1964,.T.);
#7283=EDGE_CURVE('',#8662,#8661,#9546,.T.);
#7284=EDGE_CURVE('',#8653,#8662,#1965,.T.);
#7285=EDGE_CURVE('',#8653,#8641,#9547,.T.);
#7286=EDGE_CURVE('',#8643,#8662,#9548,.T.);
#7287=EDGE_CURVE('',#8661,#8644,#9549,.T.);
#7288=EDGE_CURVE('',#8642,#8652,#9550,.T.);
#7289=EDGE_CURVE('',#8663,#8664,#9551,.T.);
#7290=EDGE_CURVE('',#8664,#8665,#992,.T.);
#7291=EDGE_CURVE('',#8665,#8666,#9552,.T.);
#7292=EDGE_CURVE('',#8666,#8663,#993,.T.);
#7293=EDGE_CURVE('',#8667,#8667,#994,.T.);
#7294=EDGE_CURVE('',#8668,#8668,#995,.T.);
#7295=EDGE_CURVE('',#8638,#8669,#9553,.T.);
#7296=EDGE_CURVE('',#8669,#8670,#996,.T.);
#7297=EDGE_CURVE('',#8670,#8637,#9554,.T.);
#7298=EDGE_CURVE('',#8635,#8671,#9555,.T.);
#7299=EDGE_CURVE('',#8671,#8672,#997,.T.);
#7300=EDGE_CURVE('',#8639,#8672,#9556,.T.);
#7301=EDGE_CURVE('',#8673,#8673,#998,.T.);
#7302=EDGE_CURVE('',#8674,#8674,#999,.T.);
#7303=EDGE_CURVE('',#8671,#8675,#9557,.T.);
#7304=EDGE_CURVE('',#8675,#8676,#1000,.T.);
#7305=EDGE_CURVE('',#8676,#8672,#9558,.T.);
#7306=EDGE_CURVE('',#8640,#8676,#9559,.T.);
#7307=EDGE_CURVE('',#8636,#8675,#9560,.T.);
#7308=EDGE_CURVE('',#8626,#8623,#1001,.T.);
#7309=EDGE_CURVE('',#8624,#8625,#1002,.T.);
#7310=EDGE_CURVE('',#8663,#8666,#1003,.T.);
#7311=EDGE_CURVE('',#8652,#8652,#1004,.T.);
#7312=EDGE_CURVE('',#8669,#8670,#1005,.T.);
#7313=EDGE_CURVE('',#8632,#8633,#1006,.T.);
#7314=EDGE_CURVE('',#8634,#8631,#1007,.T.);
#7315=EDGE_CURVE('',#8664,#8665,#1148,.T.);
#7316=EDGE_CURVE('',#8677,#8677,#1008,.T.);
#8619=VERTEX_POINT('',#41105);
#8620=VERTEX_POINT('',#41106);
#8621=VERTEX_POINT('',#41108);
#8622=VERTEX_POINT('',#41110);
#8623=VERTEX_POINT('',#41114);
#8624=VERTEX_POINT('',#41115);
#8625=VERTEX_POINT('',#41120);
#8626=VERTEX_POINT('',#41121);
#8627=VERTEX_POINT('',#41126);
#8628=VERTEX_POINT('',#41127);
#8629=VERTEX_POINT('',#41129);
#8630=VERTEX_POINT('',#41131);
#8631=VERTEX_POINT('',#41135);
#8632=VERTEX_POINT('',#41136);
#8633=VERTEX_POINT('',#41141);
#8634=VERTEX_POINT('',#41142);
#8635=VERTEX_POINT('',#41147);
#8636=VERTEX_POINT('',#41148);
#8637=VERTEX_POINT('',#41150);
#8638=VERTEX_POINT('',#41152);
#8639=VERTEX_POINT('',#41154);
#8640=VERTEX_POINT('',#41156);
#8641=VERTEX_POINT('',#41289);
#8642=VERTEX_POINT('',#41290);
#8643=VERTEX_POINT('',#41356);
#8644=VERTEX_POINT('',#41358);
#8645=VERTEX_POINT('',#41368);
#8646=VERTEX_POINT('',#41378);
#8647=VERTEX_POINT('',#41388);
#8648=VERTEX_POINT('',#41398);
#8649=VERTEX_POINT('',#41408);
#8650=VERTEX_POINT('',#41418);
#8651=VERTEX_POINT('',#41428);
#8652=VERTEX_POINT('',#41569);
#8653=VERTEX_POINT('',#41570);
#8654=VERTEX_POINT('',#41580);
#8655=VERTEX_POINT('',#41590);
#8656=VERTEX_POINT('',#41600);
#8657=VERTEX_POINT('',#41610);
#8658=VERTEX_POINT('',#41620);
#8659=VERTEX_POINT('',#41630);
#8660=VERTEX_POINT('',#41640);
#8661=VERTEX_POINT('',#41650);
#8662=VERTEX_POINT('',#41652);
#8663=VERTEX_POINT('',#41727);
#8664=VERTEX_POINT('',#41728);
#8665=VERTEX_POINT('',#41730);
#8666=VERTEX_POINT('',#41732);
#8667=VERTEX_POINT('',#41736);
#8668=VERTEX_POINT('',#41738);
#8669=VERTEX_POINT('',#41741);
#8670=VERTEX_POINT('',#41743);
#8671=VERTEX_POINT('',#41746);
#8672=VERTEX_POINT('',#41748);
#8673=VERTEX_POINT('',#41752);
#8674=VERTEX_POINT('',#41754);
#8675=VERTEX_POINT('',#41756);
#8676=VERTEX_POINT('',#41758);
#8677=VERTEX_POINT('',#41783);
#9533=LINE('',#41116,#10361);
#9534=LINE('',#41117,#10362);
#9535=LINE('',#41122,#10363);
#9536=LINE('',#41123,#10364);
#9537=LINE('',#41137,#10365);
#9538=LINE('',#41138,#10366);
#9539=LINE('',#41143,#10367);
#9540=LINE('',#41144,#10368);
#9541=LINE('',#41146,#10369);
#9542=LINE('',#41155,#10370);
#9543=LINE('',#41288,#10371);
#9544=LINE('',#41357,#10372);
#9545=LINE('',#41568,#10373);
#9546=LINE('',#41651,#10374);
#9547=LINE('',#41719,#10375);
#9548=LINE('',#41720,#10376);
#9549=LINE('',#41722,#10377);
#9550=LINE('',#41724,#10378);
#9551=LINE('',#41726,#10379);
#9552=LINE('',#41731,#10380);
#9553=LINE('',#41740,#10381);
#9554=LINE('',#41744,#10382);
#9555=LINE('',#41745,#10383);
#9556=LINE('',#41749,#10384);
#9557=LINE('',#41755,#10385);
#9558=LINE('',#41759,#10386);
#9559=LINE('',#41761,#10387);
#9560=LINE('',#41763,#10388);
#10361=VECTOR('',#18721,1.);
#10362=VECTOR('',#18722,1.);
#10363=VECTOR('',#18727,1.);
#10364=VECTOR('',#18728,1.);
#10365=VECTOR('',#18743,1.);
#10366=VECTOR('',#18744,1.);
#10367=VECTOR('',#18749,1.);
#10368=VECTOR('',#18750,1.);
#10369=VECTOR('',#18753,1.);
#10370=VECTOR('',#18760,1.);
#10371=VECTOR('',#18763,1.);
#10372=VECTOR('',#18764,1.);
#10373=VECTOR('',#18765,1.);
#10374=VECTOR('',#18766,1.);
#10375=VECTOR('',#18769,1.);
#10376=VECTOR('',#18770,1.);
#10377=VECTOR('',#18773,1.);
#10378=VECTOR('',#18776,1.);
#10379=VECTOR('',#18779,1.);
#10380=VECTOR('',#18782,1.);
#10381=VECTOR('',#18793,1.);
#10382=VECTOR('',#18796,1.);
#10383=VECTOR('',#18797,1.);
#10384=VECTOR('',#18800,1.);
#10385=VECTOR('',#18807,1.);
#10386=VECTOR('',#18810,1.);
#10387=VECTOR('',#18813,1.);
#10388=VECTOR('',#18816,1.);
#11421=EDGE_LOOP('',(#5180,#5181,#5182,#5183));
#11422=EDGE_LOOP('',(#5184,#5185,#5186,#5187));
#11423=EDGE_LOOP('',(#5188,#5189,#5190,#5191));
#11424=EDGE_LOOP('',(#5192,#5193,#5194,#5195));
#11425=EDGE_LOOP('',(#5196,#5197,#5198,#5199));
#11426=EDGE_LOOP('',(#5200,#5201,#5202,#5203));
#11427=EDGE_LOOP('',(#5204,#5205,#5206,#5207,#5208,#5209));
#11428=EDGE_LOOP('',(#5210,#5211,#5212,#5213,#5214,#5215,#5216,#5217,#5218,
#5219,#5220));
#11429=EDGE_LOOP('',(#5221,#5222,#5223,#5224,#5225,#5226,#5227,#5228,#5229,
#5230,#5231));
#11430=EDGE_LOOP('',(#5232,#5233,#5234,#5235));
#11431=EDGE_LOOP('',(#5236,#5237,#5238,#5239));
#11432=EDGE_LOOP('',(#5240,#5241,#5242,#5243));
#11433=EDGE_LOOP('',(#5244,#5245,#5246,#5247));
#11434=EDGE_LOOP('',(#5248));
#11435=EDGE_LOOP('',(#5249));
#11436=EDGE_LOOP('',(#5250,#5251,#5252,#5253,#5254,#5255,#5256,#5257));
#11437=EDGE_LOOP('',(#5258));
#11438=EDGE_LOOP('',(#5259));
#11439=EDGE_LOOP('',(#5260,#5261,#5262,#5263));
#11440=EDGE_LOOP('',(#5264,#5265,#5266,#5267));
#11441=EDGE_LOOP('',(#5268,#5269,#5270,#5271));
#11442=EDGE_LOOP('',(#5272,#5273,#5274,#5275));
#11443=EDGE_LOOP('',(#5276,#5277,#5278,#5279));
#11444=EDGE_LOOP('',(#5280,#5281));
#11445=EDGE_LOOP('',(#5282));
#11446=EDGE_LOOP('',(#5283,#5284));
#11447=EDGE_LOOP('',(#5285,#5286,#5287,#5288));
#11448=EDGE_LOOP('',(#5289,#5290,#5291,#5292,#5293,#5294,#5295,#5296,#5297,
#5298,#5299,#5300,#5301,#5302,#5303,#5304,#5305,#5306,#5307));
#11449=EDGE_LOOP('',(#5308));
#11450=EDGE_LOOP('',(#5309,#5310,#5311,#5312));
#11451=EDGE_LOOP('',(#5313));
#11452=EDGE_LOOP('',(#5314));
#11453=EDGE_LOOP('',(#5315));
#11454=EDGE_LOOP('',(#5316));
#11455=EDGE_LOOP('',(#5317,#5318));
#11456=EDGE_LOOP('',(#5319));
#11457=EDGE_LOOP('',(#5320,#5321,#5322,#5323));
#11458=EDGE_LOOP('',(#5324,#5325,#5326,#5327));
#11459=EDGE_LOOP('',(#5328,#5329,#5330,#5331));
#11460=EDGE_LOOP('',(#5332,#5333,#5334,#5335));
#11461=EDGE_LOOP('',(#5336,#5337,#5338,#5339));
#12540=FACE_BOUND('',#11421,.T.);
#12541=FACE_BOUND('',#11422,.T.);
#12542=FACE_BOUND('',#11423,.T.);
#12543=FACE_BOUND('',#11424,.T.);
#12544=FACE_BOUND('',#11425,.T.);
#12545=FACE_BOUND('',#11426,.T.);
#12546=FACE_BOUND('',#11427,.T.);
#12547=FACE_BOUND('',#11428,.T.);
#12548=FACE_BOUND('',#11429,.T.);
#12549=FACE_BOUND('',#11430,.T.);
#12550=FACE_BOUND('',#11431,.T.);
#12551=FACE_BOUND('',#11432,.T.);
#12552=FACE_BOUND('',#11433,.T.);
#12553=FACE_BOUND('',#11434,.T.);
#12554=FACE_BOUND('',#11435,.T.);
#12555=FACE_BOUND('',#11436,.T.);
#12556=FACE_BOUND('',#11437,.T.);
#12557=FACE_BOUND('',#11438,.T.);
#12558=FACE_BOUND('',#11439,.T.);
#12559=FACE_BOUND('',#11440,.T.);
#12560=FACE_BOUND('',#11441,.T.);
#12561=FACE_BOUND('',#11442,.T.);
#12562=FACE_BOUND('',#11443,.T.);
#12563=FACE_BOUND('',#11444,.T.);
#12564=FACE_BOUND('',#11445,.T.);
#12565=FACE_BOUND('',#11446,.T.);
#12566=FACE_BOUND('',#11447,.T.);
#12567=FACE_BOUND('',#11448,.T.);
#12568=FACE_BOUND('',#11449,.T.);
#12569=FACE_BOUND('',#11450,.T.);
#12570=FACE_BOUND('',#11451,.T.);
#12571=FACE_BOUND('',#11452,.T.);
#12572=FACE_BOUND('',#11453,.T.);
#12573=FACE_BOUND('',#11454,.T.);
#12574=FACE_BOUND('',#11455,.T.);
#12575=FACE_BOUND('',#11456,.T.);
#12576=FACE_BOUND('',#11457,.T.);
#12577=FACE_BOUND('',#11458,.T.);
#12578=FACE_BOUND('',#11459,.T.);
#12579=FACE_BOUND('',#11460,.T.);
#12580=FACE_BOUND('',#11461,.T.);
#12695=(
BOUNDED_SURFACE()
B_SPLINE_SURFACE(1,2,((#41158,#41159,#41160,#41161,#41162,#41163,#41164,
#41165,#41166,#41167,#41168,#41169,#41170,#41171,#41172,#41173,#41174,#41175,
#41176,#41177,#41178,#41179,#41180,#41181,#41182,#41183,#41184,#41185,#41186,
#41187,#41188,#41189,#41190,#41191,#41192,#41193,#41194,#41195,#41196,#41197,
#41198,#41199,#41200,#41201,#41202,#41203,#41204,#41205,#41206,#41207,#41208,
#41209,#41210,#41211,#41212,#41213,#41214,#41215,#41216,#41217,#41218,#41219,
#41220,#41221,#41222),(#41223,#41224,#41225,#41226,#41227,#41228,#41229,
#41230,#41231,#41232,#41233,#41234,#41235,#41236,#41237,#41238,#41239,#41240,
#41241,#41242,#41243,#41244,#41245,#41246,#41247,#41248,#41249,#41250,#41251,
#41252,#41253,#41254,#41255,#41256,#41257,#41258,#41259,#41260,#41261,#41262,
#41263,#41264,#41265,#41266,#41267,#41268,#41269,#41270,#41271,#41272,#41273,
#41274,#41275,#41276,#41277,#41278,#41279,#41280,#41281,#41282,#41283,#41284,
#41285,#41286,#41287)),.RULED_SURF.,.F.,.F.,.F.)
B_SPLINE_SURFACE_WITH_KNOTS((2,2),(3,2,2,2,2,2,2,2,2,2,2,2,2,2,2,2,2,2,
2,2,2,2,2,2,2,2,2,2,2,2,2,2,3),(0.,1.),(0.,0.03125,0.0625,0.09375,0.125,
0.15625,0.1875,0.21875,0.25,0.28125,0.3125,0.34375,0.375,0.40625,0.4375,
0.46875,0.5,0.53125,0.5625,0.59375,0.625,0.65625,0.6875,0.71875,0.75,0.78125,
0.8125,0.84375,0.875,0.90625,0.9375,0.96875,1.),.UNSPECIFIED.)
GEOMETRIC_REPRESENTATION_ITEM()
RATIONAL_B_SPLINE_SURFACE(((1.,0.923879532511287,1.,0.923879532511287,1.,
0.923879532511287,1.,0.923879532511287,1.,0.923879532511287,1.,0.923879532511287,
1.,0.923879532511287,1.,0.923879532511287,1.,0.923879532511287,1.,0.923879532511287,
1.,0.923879532511287,1.,0.923879532511287,1.,0.923879532511287,1.,0.923879532511287,
1.,0.923879532511287,1.,0.923879532511287,1.,0.923879532511287,1.,0.923879532511287,
1.,0.923879532511287,1.,0.923879532511287,1.,0.923879532511287,1.,0.923879532511287,
1.,0.923879532511287,1.,0.923879532511287,1.,0.923879532511287,1.,0.923879532511287,
1.,0.923879532511287,1.,0.923879532511287,1.,0.923879532511287,1.,0.923879532511287,
1.,0.923879532511287,1.,0.923879532511287,1.),(1.,0.923879532511287,1.,
0.923879532511287,1.,0.923879532511287,1.,0.923879532511287,1.,0.923879532511287,
1.,0.923879532511287,1.,0.923879532511287,1.,0.923879532511287,1.,0.923879532511287,
1.,0.923879532511287,1.,0.923879532511287,1.,0.923879532511287,1.,0.923879532511287,
1.,0.923879532511287,1.,0.923879532511287,1.,0.923879532511287,1.,0.923879532511287,
1.,0.923879532511287,1.,0.923879532511287,1.,0.923879532511287,1.,0.923879532511287,
1.,0.923879532511287,1.,0.923879532511287,1.,0.923879532511287,1.,0.923879532511287,
1.,0.923879532511287,1.,0.923879532511287,1.,0.923879532511287,1.,0.923879532511287,
1.,0.923879532511287,1.,0.923879532511287,1.,0.923879532511287,1.)))
REPRESENTATION_ITEM('')
SURFACE()
);
#12696=(
BOUNDED_SURFACE()
B_SPLINE_SURFACE(1,2,((#41438,#41439,#41440,#41441,#41442,#41443,#41444,
#41445,#41446,#41447,#41448,#41449,#41450,#41451,#41452,#41453,#41454,#41455,
#41456,#41457,#41458,#41459,#41460,#41461,#41462,#41463,#41464,#41465,#41466,
#41467,#41468,#41469,#41470,#41471,#41472,#41473,#41474,#41475,#41476,#41477,
#41478,#41479,#41480,#41481,#41482,#41483,#41484,#41485,#41486,#41487,#41488,
#41489,#41490,#41491,#41492,#41493,#41494,#41495,#41496,#41497,#41498,#41499,
#41500,#41501,#41502),(#41503,#41504,#41505,#41506,#41507,#41508,#41509,
#41510,#41511,#41512,#41513,#41514,#41515,#41516,#41517,#41518,#41519,#41520,
#41521,#41522,#41523,#41524,#41525,#41526,#41527,#41528,#41529,#41530,#41531,
#41532,#41533,#41534,#41535,#41536,#41537,#41538,#41539,#41540,#41541,#41542,
#41543,#41544,#41545,#41546,#41547,#41548,#41549,#41550,#41551,#41552,#41553,
#41554,#41555,#41556,#41557,#41558,#41559,#41560,#41561,#41562,#41563,#41564,
#41565,#41566,#41567)),.RULED_SURF.,.F.,.F.,.F.)
B_SPLINE_SURFACE_WITH_KNOTS((2,2),(3,2,2,2,2,2,2,2,2,2,2,2,2,2,2,2,2,2,
2,2,2,2,2,2,2,2,2,2,2,2,2,2,3),(0.,1.),(0.,0.03125,0.0625,0.09375,0.125,
0.15625,0.1875,0.21875,0.25,0.28125,0.3125,0.34375,0.375,0.40625,0.4375,
0.46875,0.5,0.53125,0.5625,0.59375,0.625,0.65625,0.6875,0.71875,0.75,0.78125,
0.8125,0.84375,0.875,0.90625,0.9375,0.96875,1.),.UNSPECIFIED.)
GEOMETRIC_REPRESENTATION_ITEM()
RATIONAL_B_SPLINE_SURFACE(((1.,0.923879532511287,1.,0.923879532511287,1.,
0.923879532511287,1.,0.923879532511287,1.,0.923879532511287,1.,0.923879532511287,
1.,0.923879532511287,1.,0.923879532511287,1.,0.923879532511287,1.,0.923879532511287,
1.,0.923879532511287,1.,0.923879532511287,1.,0.923879532511287,1.,0.923879532511287,
1.,0.923879532511287,1.,0.923879532511287,1.,0.923879532511287,1.,0.923879532511287,
1.,0.923879532511287,1.,0.923879532511287,1.,0.923879532511287,1.,0.923879532511287,
1.,0.923879532511287,1.,0.923879532511287,1.,0.923879532511287,1.,0.923879532511287,
1.,0.923879532511287,1.,0.923879532511287,1.,0.923879532511287,1.,0.923879532511287,
1.,0.923879532511287,1.,0.923879532511287,1.),(1.,0.923879532511287,1.,
0.923879532511287,1.,0.923879532511287,1.,0.923879532511287,1.,0.923879532511287,
1.,0.923879532511287,1.,0.923879532511287,1.,0.923879532511287,1.,0.923879532511287,
1.,0.923879532511287,1.,0.923879532511287,1.,0.923879532511287,1.,0.923879532511287,
1.,0.923879532511287,1.,0.923879532511287,1.,0.923879532511287,1.,0.923879532511287,
1.,0.923879532511287,1.,0.923879532511287,1.,0.923879532511287,1.,0.923879532511287,
1.,0.923879532511287,1.,0.923879532511287,1.,0.923879532511287,1.,0.923879532511287,
1.,0.923879532511287,1.,0.923879532511287,1.,0.923879532511287,1.,0.923879532511287,
1.,0.923879532511287,1.,0.923879532511287,1.,0.923879532511287,1.)))
REPRESENTATION_ITEM('')
SURFACE()
);
#13410=ADVANCED_FACE('',(#12540),#1513,.F.);
#13411=ADVANCED_FACE('',(#12541),#1792,.F.);
#13412=ADVANCED_FACE('',(#12542),#1793,.T.);
#13413=ADVANCED_FACE('',(#12543),#1514,.F.);
#13414=ADVANCED_FACE('',(#12544),#1794,.F.);
#13415=ADVANCED_FACE('',(#12545),#1795,.F.);
#13416=ADVANCED_FACE('',(#12546),#1515,.F.);
#13417=ADVANCED_FACE('',(#12547),#12695,.F.);
#13418=ADVANCED_FACE('',(#12548),#12696,.F.);
#13419=ADVANCED_FACE('',(#12549),#1796,.T.);
#13420=ADVANCED_FACE('',(#12550),#1516,.T.);
#13421=ADVANCED_FACE('',(#12551),#1517,.F.);
#13422=ADVANCED_FACE('',(#12552),#1797,.F.);
#13423=ADVANCED_FACE('',(#12553,#12554),#1518,.F.);
#13424=ADVANCED_FACE('',(#12555),#1798,.F.);
#13425=ADVANCED_FACE('',(#12556,#12557,#12558),#1519,.F.);
#13426=ADVANCED_FACE('',(#12559),#1520,.T.);
#13427=ADVANCED_FACE('',(#12560),#1521,.T.);
#13428=ADVANCED_FACE('',(#12561),#1799,.T.);
#13429=ADVANCED_FACE('',(#12562,#12563,#12564,#12565,#12566),#1522,.T.);
#13430=ADVANCED_FACE('',(#12567,#12568),#1800,.T.);
#13431=ADVANCED_FACE('',(#12569),#1801,.F.);
#13432=ADVANCED_FACE('',(#12570,#12571),#1802,.F.);
#13433=ADVANCED_FACE('',(#12572,#12573),#1803,.F.);
#13434=ADVANCED_FACE('',(#12574,#12575),#31,.F.);
#13435=ADVANCED_FACE('',(#12576),#1804,.T.);
#13436=ADVANCED_FACE('',(#12577),#1805,.F.);
#13437=ADVANCED_FACE('',(#12578),#1806,.T.);
#13438=ADVANCED_FACE('',(#12579),#1807,.F.);
#13439=ADVANCED_FACE('',(#12580),#1808,.F.);
#13525=CLOSED_SHELL('',(#13410,#13411,#13412,#13413,#13414,#13415,#13416,
#13417,#13418,#13419,#13420,#13421,#13422,#13423,#13424,#13425,#13426,#13427,
#13428,#13429,#13430,#13431,#13432,#13433,#13434,#13435,#13436,#13437,#13438,
#13439));
#13552=STYLED_ITEM('',(#13579),#13742);
#13579=PRESENTATION_STYLE_ASSIGNMENT((#13606));
#13606=SURFACE_STYLE_USAGE(.BOTH.,#13633);
#13633=SURFACE_SIDE_STYLE('',(#13660));
#13660=SURFACE_STYLE_FILL_AREA(#13687);
#13687=FILL_AREA_STYLE('',(#13714));
#13714=FILL_AREA_STYLE_COLOUR('',#60);
#13742=MANIFOLD_SOLID_BREP('refill_port',#13525);
#13770=SHAPE_DEFINITION_REPRESENTATION(#45577,#13798);
#13798=SHAPE_REPRESENTATION('refill_port',(#13802),#45488);
#13802=AXIS2_PLACEMENT_3D('',#19109,#15295,#15296);
#15128=AXIS2_PLACEMENT_3D('',#41103,#18707,#18708);
#15129=AXIS2_PLACEMENT_3D('',#41104,#18709,#18710);
#15130=AXIS2_PLACEMENT_3D('',#41107,#18711,#18712);
#15131=AXIS2_PLACEMENT_3D('',#41109,#18713,#18714);
#15132=AXIS2_PLACEMENT_3D('',#41111,#18715,#18716);
#15133=AXIS2_PLACEMENT_3D('',#41112,#18717,#18718);
#15134=AXIS2_PLACEMENT_3D('',#41113,#18719,#18720);
#15135=AXIS2_PLACEMENT_3D('',#41118,#18723,#18724);
#15136=AXIS2_PLACEMENT_3D('',#41119,#18725,#18726);
#15137=AXIS2_PLACEMENT_3D('',#41124,#18729,#18730);
#15138=AXIS2_PLACEMENT_3D('',#41125,#18731,#18732);
#15139=AXIS2_PLACEMENT_3D('',#41128,#18733,#18734);
#15140=AXIS2_PLACEMENT_3D('',#41130,#18735,#18736);
#15141=AXIS2_PLACEMENT_3D('',#41132,#18737,#18738);
#15142=AXIS2_PLACEMENT_3D('',#41133,#18739,#18740);
#15143=AXIS2_PLACEMENT_3D('',#41134,#18741,#18742);
#15144=AXIS2_PLACEMENT_3D('',#41139,#18745,#18746);
#15145=AXIS2_PLACEMENT_3D('',#41140,#18747,#18748);
#15146=AXIS2_PLACEMENT_3D('',#41145,#18751,#18752);
#15147=AXIS2_PLACEMENT_3D('',#41149,#18754,#18755);
#15148=AXIS2_PLACEMENT_3D('',#41151,#18756,#18757);
#15149=AXIS2_PLACEMENT_3D('',#41153,#18758,#18759);
#15150=AXIS2_PLACEMENT_3D('',#41157,#18761,#18762);
#15151=AXIS2_PLACEMENT_3D('',#41718,#18767,#18768);
#15152=AXIS2_PLACEMENT_3D('',#41721,#18771,#18772);
#15153=AXIS2_PLACEMENT_3D('',#41723,#18774,#18775);
#15154=AXIS2_PLACEMENT_3D('',#41725,#18777,#18778);
#15155=AXIS2_PLACEMENT_3D('',#41729,#18780,#18781);
#15156=AXIS2_PLACEMENT_3D('',#41733,#18783,#18784);
#15157=AXIS2_PLACEMENT_3D('',#41734,#18785,#18786);
#15158=AXIS2_PLACEMENT_3D('',#41735,#18787,#18788);
#15159=AXIS2_PLACEMENT_3D('',#41737,#18789,#18790);
#15160=AXIS2_PLACEMENT_3D('',#41739,#18791,#18792);
#15161=AXIS2_PLACEMENT_3D('',#41742,#18794,#18795);
#15162=AXIS2_PLACEMENT_3D('',#41747,#18798,#18799);
#15163=AXIS2_PLACEMENT_3D('',#41750,#18801,#18802);
#15164=AXIS2_PLACEMENT_3D('',#41751,#18803,#18804);
#15165=AXIS2_PLACEMENT_3D('',#41753,#18805,#18806);
#15166=AXIS2_PLACEMENT_3D('',#41757,#18808,#18809);
#15167=AXIS2_PLACEMENT_3D('',#41760,#18811,#18812);
#15168=AXIS2_PLACEMENT_3D('',#41762,#18814,#18815);
#15169=AXIS2_PLACEMENT_3D('',#41764,#18817,#18818);
#15170=AXIS2_PLACEMENT_3D('',#41765,#18819,#18820);
#15171=AXIS2_PLACEMENT_3D('',#41766,#18821,#18822);
#15172=AXIS2_PLACEMENT_3D('',#41767,#18823,#18824);
#15173=AXIS2_PLACEMENT_3D('',#41768,#18825,#18826);
#15174=AXIS2_PLACEMENT_3D('',#41769,#18827,#18828);
#15175=AXIS2_PLACEMENT_3D('',#41770,#18829,#18830);
#15176=AXIS2_PLACEMENT_3D('',#41771,#18831,#18832);
#15177=AXIS2_PLACEMENT_3D('',#41772,#18833,#18834);
#15178=AXIS2_PLACEMENT_3D('',#41773,#18835,#18836);
#15179=AXIS2_PLACEMENT_3D('',#41774,#18837,#18838);
#15180=AXIS2_PLACEMENT_3D('',#41780,#18839,#18840);
#15181=AXIS2_PLACEMENT_3D('',#41781,#18841,#18842);
#15182=AXIS2_PLACEMENT_3D('',#41782,#18843,#18844);
#15183=AXIS2_PLACEMENT_3D('',#41784,#18845,#18846);
#15184=AXIS2_PLACEMENT_3D('',#41785,#18847,#18848);
#15185=AXIS2_PLACEMENT_3D('',#41786,#18849,#18850);
#15186=AXIS2_PLACEMENT_3D('',#41787,#18851,#18852);
#15187=AXIS2_PLACEMENT_3D('',#41788,#18853,#18854);
#15188=AXIS2_PLACEMENT_3D('',#41789,#18855,#18856);
#15295=DIRECTION('',(0.,0.,1.));
#15296=DIRECTION('',(1.,0.,0.));
#18707=DIRECTION('',(0.,0.,1.));
#18708=DIRECTION('',(1.,0.,0.));
#18709=DIRECTION('',(0.,0.,1.));
#18710=DIRECTION('',(-1.,0.,0.));
#18711=DIRECTION('',(0.,0.,-1.));
#18712=DIRECTION('',(-1.,0.,0.));
#18713=DIRECTION('',(0.,0.,-1.));
#18714=DIRECTION('',(-1.,0.,0.));
#18715=DIRECTION('',(0.,0.,-1.));
#18716=DIRECTION('',(-1.,0.,0.));
#18717=DIRECTION('',(0.,0.,-1.));
#18718=DIRECTION('',(-1.,0.,0.));
#18719=DIRECTION('',(0.,0.,-1.));
#18720=DIRECTION('',(-1.,0.,0.));
#18721=DIRECTION('',(0.,0.,-1.));
#18722=DIRECTION('',(0.,0.,-1.));
#18723=DIRECTION('',(0.,0.,-1.));
#18724=DIRECTION('',(-1.,0.,0.));
#18725=DIRECTION('',(0.,0.,1.));
#18726=DIRECTION('',(-1.,0.,0.));
#18727=DIRECTION('',(0.,0.,-1.));
#18728=DIRECTION('',(0.,0.,-1.));
#18729=DIRECTION('',(0.,0.,1.));
#18730=DIRECTION('',(1.,0.,0.));
#18731=DIRECTION('',(0.,0.,-1.));
#18732=DIRECTION('',(1.,0.,0.));
#18733=DIRECTION('',(0.,0.,1.));
#18734=DIRECTION('',(1.,0.,0.));
#18735=DIRECTION('',(0.,0.,-1.));
#18736=DIRECTION('',(1.,0.,0.));
#18737=DIRECTION('',(0.,0.,-1.));
#18738=DIRECTION('',(1.,0.,0.));
#18739=DIRECTION('',(0.,0.,-1.));
#18740=DIRECTION('',(-1.,0.,0.));
#18741=DIRECTION('',(0.,0.,-1.));
#18742=DIRECTION('',(1.,0.,0.));
#18743=DIRECTION('',(0.,0.,-1.));
#18744=DIRECTION('',(0.,0.,-1.));
#18745=DIRECTION('',(0.,0.,-1.));
#18746=DIRECTION('',(-1.,0.,0.));
#18747=DIRECTION('',(0.,0.,-1.));
#18748=DIRECTION('',(1.,0.,0.));
#18749=DIRECTION('',(0.,0.,-1.));
#18750=DIRECTION('',(0.,0.,-1.));
#18751=DIRECTION('',(0.,0.,-1.));
#18752=DIRECTION('',(-1.,0.,0.));
#18753=DIRECTION('',(-1.,0.,0.));
#18754=DIRECTION('',(0.,0.,1.));
#18755=DIRECTION('',(-1.,0.,0.));
#18756=DIRECTION('',(0.,0.,-1.));
#18757=DIRECTION('',(-1.,0.,0.));
#18758=DIRECTION('',(0.,0.,1.));
#18759=DIRECTION('',(-1.,1.25767452008318E-14,0.));
#18760=DIRECTION('',(1.,0.,0.));
#18761=DIRECTION('',(0.,0.,-1.));
#18762=DIRECTION('',(-1.,0.,0.));
#18763=DIRECTION('',(-0.866025403784441,0.,0.5));
#18764=DIRECTION('',(0.866025403784441,0.,-0.5));
#18765=DIRECTION('',(0.866025403784439,0.,0.5));
#18766=DIRECTION('',(-0.866025403784439,0.,-0.5));
#18767=DIRECTION('',(0.,0.,1.));
#18768=DIRECTION('',(1.,0.,0.));
#18769=DIRECTION('',(0.,0.,1.));
#18770=DIRECTION('',(0.,0.,-1.));
#18771=DIRECTION('',(0.,1.,0.));
#18772=DIRECTION('',(0.,0.,1.));
#18773=DIRECTION('',(0.,0.,1.));
#18774=DIRECTION('',(0.,1.,0.));
#18775=DIRECTION('',(0.,0.,1.));
#18776=DIRECTION('',(0.,0.,-1.));
#18777=DIRECTION('',(0.,0.,1.));
#18778=DIRECTION('',(1.,0.,0.));
#18779=DIRECTION('',(1.15824759844129E-16,0.,1.));
#18780=DIRECTION('',(1.15824759844129E-16,0.,1.));
#18781=DIRECTION('',(1.,0.,0.));
#18782=DIRECTION('',(-1.15824759844129E-16,0.,-1.));
#18783=DIRECTION('',(0.,0.,-1.));
#18784=DIRECTION('',(-1.,0.,0.));
#18785=DIRECTION('',(0.,0.,-1.));
#18786=DIRECTION('',(-1.,0.,0.));
#18787=DIRECTION('',(0.,0.,1.));
#18788=DIRECTION('',(-1.,0.,0.));
#18789=DIRECTION('',(1.15824759844129E-16,0.,1.));
#18790=DIRECTION('',(1.,0.,0.));
#18791=DIRECTION('',(0.,0.,1.));
#18792=DIRECTION('',(1.,0.,0.));
#18793=DIRECTION('',(0.,0.,-1.));
#18794=DIRECTION('',(0.,0.,-1.));
#18795=DIRECTION('',(-1.,0.,0.));
#18796=DIRECTION('',(0.,0.,1.));
#18797=DIRECTION('',(0.,0.,1.));
#18798=DIRECTION('',(0.,0.,1.));
#18799=DIRECTION('',(1.,0.,0.));
#18800=DIRECTION('',(0.,0.,1.));
#18801=DIRECTION('',(0.,0.,-1.));
#18802=DIRECTION('',(-1.,0.,0.));
#18803=DIRECTION('',(0.,0.,1.));
#18804=DIRECTION('',(1.,0.,0.));
#18805=DIRECTION('',(0.,0.,-1.));
#18806=DIRECTION('',(-1.,0.,0.));
#18807=DIRECTION('',(-1.,0.,0.));
#18808=DIRECTION('',(0.,0.,1.));
#18809=DIRECTION('',(1.,0.,0.));
#18810=DIRECTION('',(1.,0.,0.));
#18811=DIRECTION('',(0.,-1.,0.));
#18812=DIRECTION('',(0.,0.,-1.));
#18813=DIRECTION('',(0.,0.,1.));
#18814=DIRECTION('',(0.,1.,0.));
#18815=DIRECTION('',(0.,0.,1.));
#18816=DIRECTION('',(0.,0.,1.));
#18817=DIRECTION('',(0.,0.,1.));
#18818=DIRECTION('',(1.,0.,0.));
#18819=DIRECTION('',(0.,0.,-1.));
#18820=DIRECTION('',(-1.,0.,0.));
#18821=DIRECTION('',(0.,0.,-1.));
#18822=DIRECTION('',(-1.,0.,0.));
#18823=DIRECTION('',(0.,0.,-1.));
#18824=DIRECTION('',(-1.,0.,0.));
#18825=DIRECTION('',(0.,0.,-1.));
#18826=DIRECTION('',(-1.,0.,0.));
#18827=DIRECTION('',(0.,0.,-1.));
#18828=DIRECTION('',(-1.,0.,0.));
#18829=DIRECTION('',(0.,0.,-1.));
#18830=DIRECTION('',(-1.,0.,0.));
#18831=DIRECTION('',(0.,0.,-1.));
#18832=DIRECTION('',(1.,0.,0.));
#18833=DIRECTION('',(0.,0.,1.));
#18834=DIRECTION('',(1.,0.,0.));
#18835=DIRECTION('',(0.,0.,-1.));
#18836=DIRECTION('',(-1.,0.,0.));
#18837=DIRECTION('',(0.,0.,1.));
#18838=DIRECTION('',(1.,0.,0.));
#18839=DIRECTION('',(0.,0.,1.));
#18840=DIRECTION('',(1.,0.,0.));
#18841=DIRECTION('',(0.,0.,1.));
#18842=DIRECTION('',(1.,0.,0.));
#18843=DIRECTION('',(1.15824759844129E-16,0.,1.));
#18844=DIRECTION('',(1.,0.,0.));
#18845=DIRECTION('',(0.,0.,-1.));
#18846=DIRECTION('',(-1.,0.,0.));
#18847=DIRECTION('',(0.,0.,-1.));
#18848=DIRECTION('',(-1.,0.,0.));
#18849=DIRECTION('',(0.,0.,-1.));
#18850=DIRECTION('',(-1.,0.,0.));
#18851=DIRECTION('',(0.,0.,-1.));
#18852=DIRECTION('',(-1.,0.,0.));
#18853=DIRECTION('',(0.,0.,-1.));
#18854=DIRECTION('',(-1.,0.,0.));
#18855=DIRECTION('',(0.,0.,-1.));
#18856=DIRECTION('',(-1.,0.,0.));
#19109=CARTESIAN_POINT('',(0.,0.,0.));
#41103=CARTESIAN_POINT('',(-0.012852081728299,0.0305608891324553,0.026));
#41104=CARTESIAN_POINT('',(-0.0115,0.0303108891324553,0.026));
#41105=CARTESIAN_POINT('',(-0.0092649160435001,0.0298976219627052,0.026));
#41106=CARTESIAN_POINT('',(-0.0092649160435001,0.0307241563022055,0.026));
#41107=CARTESIAN_POINT('',(-0.00879583654340205,0.0308108891324553,0.026));
#41108=CARTESIAN_POINT('',(-0.00832675704330399,0.0308976219627052,0.026));
#41109=CARTESIAN_POINT('',(-0.0115,0.0303108891324553,0.026));
#41110=CARTESIAN_POINT('',(-0.008326757043304,0.0297241563022054,0.026));
#41111=CARTESIAN_POINT('',(-0.00879583654340205,0.0298108891324554,0.026));
#41112=CARTESIAN_POINT('',(-0.0115,0.0303108891324553,0.026));
#41113=CARTESIAN_POINT('',(-0.0115,0.0303108891324553,0.021));
#41114=CARTESIAN_POINT('',(-0.008326757043304,0.0308976219627052,0.021));
#41115=CARTESIAN_POINT('',(-0.00832675704330399,0.0297241563022054,0.021));
#41116=CARTESIAN_POINT('',(-0.008326757043304,0.0297241563022054,0.026));
#41117=CARTESIAN_POINT('',(-0.008326757043304,0.0308976219627052,0.026));
#41118=CARTESIAN_POINT('',(-0.0115,0.0303108891324553,0.026));
#41119=CARTESIAN_POINT('',(-0.0115,0.0303108891324553,0.021));
#41120=CARTESIAN_POINT('',(-0.0092649160435001,0.0298976219627052,0.021));
#41121=CARTESIAN_POINT('',(-0.0092649160435001,0.0307241563022055,0.021));
#41122=CARTESIAN_POINT('',(-0.0092649160435001,0.0307241563022055,0.026));
#41123=CARTESIAN_POINT('',(-0.0092649160435001,0.0298976219627052,0.026));
#41124=CARTESIAN_POINT('',(-0.012852081728299,0.0305608891324553,0.026));
#41125=CARTESIAN_POINT('',(-0.014204163456598,0.0308108891324553,0.026));
#41126=CARTESIAN_POINT('',(-0.0146732429566961,0.0308976219627052,0.026));
#41127=CARTESIAN_POINT('',(-0.0137350839565,0.0307241563022055,0.026));
#41128=CARTESIAN_POINT('',(-0.0115,0.0303108891324553,0.026));
#41129=CARTESIAN_POINT('',(-0.0137350839565,0.0298976219627052,0.026));
#41130=CARTESIAN_POINT('',(-0.014204163456598,0.0298108891324554,0.026));
#41131=CARTESIAN_POINT('',(-0.0146732429566961,0.0297241563022054,0.026));
#41132=CARTESIAN_POINT('',(-0.0115,0.0303108891324553,0.026));
#41133=CARTESIAN_POINT('',(-0.014204163456598,0.0298108891324554,0.026));
#41134=CARTESIAN_POINT('',(-0.014204163456598,0.0298108891324554,0.021));
#41135=CARTESIAN_POINT('',(-0.0137350839565,0.0298976219627052,0.021));
#41136=CARTESIAN_POINT('',(-0.0146732429566961,0.0297241563022054,0.021));
#41137=CARTESIAN_POINT('',(-0.0146732429566961,0.0297241563022054,0.026));
#41138=CARTESIAN_POINT('',(-0.0137350839565,0.0298976219627052,0.026));
#41139=CARTESIAN_POINT('',(-0.014204163456598,0.0308108891324553,0.026));
#41140=CARTESIAN_POINT('',(-0.014204163456598,0.0308108891324553,0.021));
#41141=CARTESIAN_POINT('',(-0.0146732429566961,0.0308976219627052,0.021));
#41142=CARTESIAN_POINT('',(-0.0137350839565,0.0307241563022055,0.021));
#41143=CARTESIAN_POINT('',(-0.0137350839565,0.0307241563022055,0.026));
#41144=CARTESIAN_POINT('',(-0.0146732429566961,0.0308976219627052,0.026));
#41145=CARTESIAN_POINT('',(-0.0115,0.0303108891324553,0.031));
#41146=CARTESIAN_POINT('',(-0.0115,0.0328108891324553,0.031));
#41147=CARTESIAN_POINT('',(-0.0099006579232147,0.0328108891324553,0.031));
#41148=CARTESIAN_POINT('',(-0.0115,0.0328108891324553,0.031));
#41149=CARTESIAN_POINT('',(-0.0175,0.0303108891324553,0.031));
#41150=CARTESIAN_POINT('',(-0.0101875,0.0335554759705597,0.031));
#41151=CARTESIAN_POINT('',(-0.0115,0.0303108891324553,0.031));
#41152=CARTESIAN_POINT('',(-0.0101875,0.027066302294351,0.031));
#41153=CARTESIAN_POINT('',(-0.0175,0.0303108891324553,0.031));
#41154=CARTESIAN_POINT('',(-0.0099006579232147,0.0278108891324554,0.031));
#41155=CARTESIAN_POINT('',(-0.0115,0.0278108891324554,0.031));
#41156=CARTESIAN_POINT('',(-0.0115,0.0278108891324554,0.031));
#41157=CARTESIAN_POINT('',(-0.0115,0.0303108891324553,0.031));
#41158=CARTESIAN_POINT('',(-0.00678810118750004,0.0303108891324553,0.0216562499979516));
#41159=CARTESIAN_POINT('',(-0.00678810118750004,0.0347479028993611,0.0217499999979516));
#41160=CARTESIAN_POINT('',(-0.00992554371029717,0.0378853454221582,0.0218437499979516));
#41161=CARTESIAN_POINT('',(-0.0130629862330943,0.0410227879449553,0.0219374999979516));
#41162=CARTESIAN_POINT('',(-0.0175,0.0410227879449554,0.0220312499979516));
#41163=CARTESIAN_POINT('',(-0.0219370137669058,0.0410227879449553,0.0221249999979516));
#41164=CARTESIAN_POINT('',(-0.025074456289703,0.0378853454221582,0.0222187499979516));
#41165=CARTESIAN_POINT('',(-0.0282118988125001,0.0347479028993611,0.0223124999979516));
#41166=CARTESIAN_POINT('',(-0.0282118988125,0.0303108891324553,0.0224062499979516));
#41167=CARTESIAN_POINT('',(-0.0282118988125001,0.0258738753655496,0.0224999999979516));
#41168=CARTESIAN_POINT('',(-0.025074456289703,0.0227364328427525,0.0225937499979516));
#41169=CARTESIAN_POINT('',(-0.0219370137669058,0.0195989903199553,0.0226874999979516));
#41170=CARTESIAN_POINT('',(-0.0175,0.0195989903199554,0.0227812499979516));
#41171=CARTESIAN_POINT('',(-0.0130629862330943,0.0195989903199553,0.0228749999979516));
#41172=CARTESIAN_POINT('',(-0.00992554371029717,0.0227364328427525,0.0229687499979516));
#41173=CARTESIAN_POINT('',(-0.00678810118750004,0.0258738753655496,0.0230624999979516));
#41174=CARTESIAN_POINT('',(-0.00678810118750004,0.0303108891324553,0.0231562499979516));
#41175=CARTESIAN_POINT('',(-0.00678810118750004,0.0347479028993611,0.0232499999979516));
#41176=CARTESIAN_POINT('',(-0.00992554371029717,0.0378853454221582,0.0233437499979516));
#41177=CARTESIAN_POINT('',(-0.0130629862330943,0.0410227879449553,0.0234374999979516));
#41178=CARTESIAN_POINT('',(-0.0175,0.0410227879449554,0.0235312499979516));
#41179=CARTESIAN_POINT('',(-0.0219370137669058,0.0410227879449553,0.0236249999979516));
#41180=CARTESIAN_POINT('',(-0.025074456289703,0.0378853454221582,0.0237187499979516));
#41181=CARTESIAN_POINT('',(-0.0282118988125001,0.0347479028993611,0.0238124999979516));
#41182=CARTESIAN_POINT('',(-0.0282118988125,0.0303108891324553,0.0239062499979516));
#41183=CARTESIAN_POINT('',(-0.0282118988125001,0.0258738753655496,0.0239999999979516));
#41184=CARTESIAN_POINT('',(-0.025074456289703,0.0227364328427525,0.0240937499979516));
#41185=CARTESIAN_POINT('',(-0.0219370137669058,0.0195989903199553,0.0241874999979516));
#41186=CARTESIAN_POINT('',(-0.0175,0.0195989903199554,0.0242812499979516));
#41187=CARTESIAN_POINT('',(-0.0130629862330943,0.0195989903199553,0.0243749999979516));
#41188=CARTESIAN_POINT('',(-0.00992554371029717,0.0227364328427525,0.0244687499979516));
#41189=CARTESIAN_POINT('',(-0.00678810118750004,0.0258738753655496,0.0245624999979516));
#41190=CARTESIAN_POINT('',(-0.00678810118750004,0.0303108891324553,0.0246562499979516));
#41191=CARTESIAN_POINT('',(-0.00678810118750004,0.0347479028993611,0.0247499999979516));
#41192=CARTESIAN_POINT('',(-0.00992554371029717,0.0378853454221582,0.0248437499979516));
#41193=CARTESIAN_POINT('',(-0.0130629862330943,0.0410227879449553,0.0249374999979516));
#41194=CARTESIAN_POINT('',(-0.0175,0.0410227879449554,0.0250312499979516));
#41195=CARTESIAN_POINT('',(-0.0219370137669058,0.0410227879449553,0.0251249999979516));
#41196=CARTESIAN_POINT('',(-0.025074456289703,0.0378853454221582,0.0252187499979516));
#41197=CARTESIAN_POINT('',(-0.0282118988125001,0.0347479028993611,0.0253124999979516));
#41198=CARTESIAN_POINT('',(-0.0282118988125,0.0303108891324553,0.0254062499979516));
#41199=CARTESIAN_POINT('',(-0.0282118988125001,0.0258738753655496,0.0254999999979516));
#41200=CARTESIAN_POINT('',(-0.025074456289703,0.0227364328427525,0.0255937499979516));
#41201=CARTESIAN_POINT('',(-0.0219370137669058,0.0195989903199553,0.0256874999979516));
#41202=CARTESIAN_POINT('',(-0.0175,0.0195989903199554,0.0257812499979516));
#41203=CARTESIAN_POINT('',(-0.0130629862330943,0.0195989903199553,0.0258749999979516));
#41204=CARTESIAN_POINT('',(-0.00992554371029717,0.0227364328427525,0.0259687499979516));
#41205=CARTESIAN_POINT('',(-0.00678810118750004,0.0258738753655496,0.0260624999979516));
#41206=CARTESIAN_POINT('',(-0.00678810118750004,0.0303108891324553,0.0261562499979516));
#41207=CARTESIAN_POINT('',(-0.00678810118750004,0.0347479028993611,0.0262499999979516));
#41208=CARTESIAN_POINT('',(-0.00992554371029717,0.0378853454221582,0.0263437499979516));
#41209=CARTESIAN_POINT('',(-0.0130629862330943,0.0410227879449553,0.0264374999979516));
#41210=CARTESIAN_POINT('',(-0.0175,0.0410227879449554,0.0265312499979516));
#41211=CARTESIAN_POINT('',(-0.0219370137669058,0.0410227879449553,0.0266249999979516));
#41212=CARTESIAN_POINT('',(-0.025074456289703,0.0378853454221582,0.0267187499979516));
#41213=CARTESIAN_POINT('',(-0.0282118988125001,0.0347479028993611,0.0268124999979516));
#41214=CARTESIAN_POINT('',(-0.0282118988125,0.0303108891324553,0.0269062499979516));
#41215=CARTESIAN_POINT('',(-0.0282118988125001,0.0258738753655496,0.0269999999979516));
#41216=CARTESIAN_POINT('',(-0.025074456289703,0.0227364328427525,0.0270937499979516));
#41217=CARTESIAN_POINT('',(-0.0219370137669058,0.0195989903199553,0.0271874999979516));
#41218=CARTESIAN_POINT('',(-0.0175,0.0195989903199554,0.0272812499979516));
#41219=CARTESIAN_POINT('',(-0.0130629862330943,0.0195989903199553,0.0273749999979516));
#41220=CARTESIAN_POINT('',(-0.00992554371029717,0.0227364328427525,0.0274687499979516));
#41221=CARTESIAN_POINT('',(-0.00678810118750004,0.0258738753655496,0.0275624999979516));
#41222=CARTESIAN_POINT('',(-0.00678810118750004,0.0303108891324553,0.0276562499979516));
#41223=CARTESIAN_POINT('',(-0.0076,0.0303108891324553,0.0221249999959033));
#41224=CARTESIAN_POINT('',(-0.00760000000000004,0.0344116033999489,0.0222187499959032));
#41225=CARTESIAN_POINT('',(-0.0104996428662532,0.0373112462662021,0.0223124999959033));
#41226=CARTESIAN_POINT('',(-0.0133992857325064,0.0402108891324553,0.0224062499959032));
#41227=CARTESIAN_POINT('',(-0.0175,0.0402108891324554,0.0224999999959033));
#41228=CARTESIAN_POINT('',(-0.0216007142674937,0.0402108891324553,0.0225937499959032));
#41229=CARTESIAN_POINT('',(-0.0245003571337469,0.0373112462662021,0.0226874999959033));
#41230=CARTESIAN_POINT('',(-0.0274,0.0344116033999489,0.0227812499959032));
#41231=CARTESIAN_POINT('',(-0.0274,0.0303108891324553,0.0228749999959033));
#41232=CARTESIAN_POINT('',(-0.0274,0.0262101748649617,0.0229687499959032));
#41233=CARTESIAN_POINT('',(-0.0245003571337469,0.0233105319987085,0.0230624999959032));
#41234=CARTESIAN_POINT('',(-0.0216007142674937,0.0204108891324553,0.0231562499959032));
#41235=CARTESIAN_POINT('',(-0.0175,0.0204108891324553,0.0232499999959032));
#41236=CARTESIAN_POINT('',(-0.0133992857325064,0.0204108891324553,0.0233437499959032));
#41237=CARTESIAN_POINT('',(-0.0104996428662532,0.0233105319987085,0.0234374999959032));
#41238=CARTESIAN_POINT('',(-0.00760000000000004,0.0262101748649617,0.0235312499959032));
#41239=CARTESIAN_POINT('',(-0.0076,0.0303108891324553,0.0236249999959032));
#41240=CARTESIAN_POINT('',(-0.00760000000000004,0.0344116033999489,0.0237187499959032));
#41241=CARTESIAN_POINT('',(-0.0104996428662532,0.0373112462662021,0.0238124999959032));
#41242=CARTESIAN_POINT('',(-0.0133992857325064,0.0402108891324553,0.0239062499959032));
#41243=CARTESIAN_POINT('',(-0.0175,0.0402108891324554,0.0239999999959032));
#41244=CARTESIAN_POINT('',(-0.0216007142674937,0.0402108891324553,0.0240937499959032));
#41245=CARTESIAN_POINT('',(-0.0245003571337469,0.0373112462662021,0.0241874999959032));
#41246=CARTESIAN_POINT('',(-0.0274,0.0344116033999489,0.0242812499959032));
#41247=CARTESIAN_POINT('',(-0.0274,0.0303108891324553,0.0243749999959032));
#41248=CARTESIAN_POINT('',(-0.0274,0.0262101748649617,0.0244687499959032));
#41249=CARTESIAN_POINT('',(-0.0245003571337469,0.0233105319987085,0.0245624999959033));
#41250=CARTESIAN_POINT('',(-0.0216007142674937,0.0204108891324553,0.0246562499959032));
#41251=CARTESIAN_POINT('',(-0.0175,0.0204108891324553,0.0247499999959033));
#41252=CARTESIAN_POINT('',(-0.0133992857325064,0.0204108891324553,0.0248437499959032));
#41253=CARTESIAN_POINT('',(-0.0104996428662532,0.0233105319987085,0.0249374999959033));
#41254=CARTESIAN_POINT('',(-0.00760000000000004,0.0262101748649617,0.0250312499959032));
#41255=CARTESIAN_POINT('',(-0.0076,0.0303108891324553,0.0251249999959033));
#41256=CARTESIAN_POINT('',(-0.00760000000000004,0.0344116033999489,0.0252187499959032));
#41257=CARTESIAN_POINT('',(-0.0104996428662532,0.0373112462662021,0.0253124999959033));
#41258=CARTESIAN_POINT('',(-0.0133992857325064,0.0402108891324553,0.0254062499959032));
#41259=CARTESIAN_POINT('',(-0.0175,0.0402108891324554,0.0254999999959033));
#41260=CARTESIAN_POINT('',(-0.0216007142674937,0.0402108891324553,0.0255937499959032));
#41261=CARTESIAN_POINT('',(-0.0245003571337469,0.0373112462662021,0.0256874999959033));
#41262=CARTESIAN_POINT('',(-0.0274,0.0344116033999489,0.0257812499959032));
#41263=CARTESIAN_POINT('',(-0.0274,0.0303108891324553,0.0258749999959033));
#41264=CARTESIAN_POINT('',(-0.0274,0.0262101748649617,0.0259687499959032));
#41265=CARTESIAN_POINT('',(-0.0245003571337469,0.0233105319987085,0.0260624999959033));
#41266=CARTESIAN_POINT('',(-0.0216007142674937,0.0204108891324553,0.0261562499959032));
#41267=CARTESIAN_POINT('',(-0.0175,0.0204108891324553,0.0262499999959033));
#41268=CARTESIAN_POINT('',(-0.0133992857325064,0.0204108891324553,0.0263437499959032));
#41269=CARTESIAN_POINT('',(-0.0104996428662532,0.0233105319987085,0.0264374999959033));
#41270=CARTESIAN_POINT('',(-0.00760000000000004,0.0262101748649617,0.0265312499959032));
#41271=CARTESIAN_POINT('',(-0.0076,0.0303108891324553,0.0266249999959033));
#41272=CARTESIAN_POINT('',(-0.00760000000000004,0.0344116033999489,0.0267187499959032));
#41273=CARTESIAN_POINT('',(-0.0104996428662532,0.0373112462662021,0.0268124999959033));
#41274=CARTESIAN_POINT('',(-0.0133992857325064,0.0402108891324553,0.0269062499959032));
#41275=CARTESIAN_POINT('',(-0.0175,0.0402108891324554,0.0269999999959032));
#41276=CARTESIAN_POINT('',(-0.0216007142674937,0.0402108891324553,0.0270937499959032));
#41277=CARTESIAN_POINT('',(-0.0245003571337469,0.0373112462662021,0.0271874999959032));
#41278=CARTESIAN_POINT('',(-0.0274,0.0344116033999489,0.0272812499959032));
#41279=CARTESIAN_POINT('',(-0.0274,0.0303108891324553,0.0273749999959032));
#41280=CARTESIAN_POINT('',(-0.0274,0.0262101748649617,0.0274687499959032));
#41281=CARTESIAN_POINT('',(-0.0245003571337469,0.0233105319987085,0.0275624999959032));
#41282=CARTESIAN_POINT('',(-0.0216007142674937,0.0204108891324553,0.0276562499959032));
#41283=CARTESIAN_POINT('',(-0.0175,0.0204108891324553,0.0277499999959032));
#41284=CARTESIAN_POINT('',(-0.0133992857325064,0.0204108891324553,0.0278437499959032));
#41285=CARTESIAN_POINT('',(-0.0104996428662532,0.0233105319987085,0.0279374999959032));
#41286=CARTESIAN_POINT('',(-0.00760000000000004,0.0262101748649617,0.0280312499959032));
#41287=CARTESIAN_POINT('',(-0.0076,0.0303108891324553,0.0281249999959032));
#41288=CARTESIAN_POINT('',(-0.00719405059375004,0.0303108891324553,0.0218906249969274));
#41289=CARTESIAN_POINT('',(-0.00678810118750004,0.0303108891324553,0.0216562499979516));
#41290=CARTESIAN_POINT('',(-0.0076,0.0303108891324553,0.0221249999959033));
#41291=CARTESIAN_POINT('',(-0.00678810118750004,0.0303108891324553,0.0216562499979516));
#41292=CARTESIAN_POINT('',(-0.00678810118750004,0.0347479028993611,0.0217499999979516));
#41293=CARTESIAN_POINT('',(-0.00992554371029717,0.0378853454221582,0.0218437499979516));
#41294=CARTESIAN_POINT('',(-0.0130629862330943,0.0410227879449553,0.0219374999979516));
#41295=CARTESIAN_POINT('',(-0.0175,0.0410227879449554,0.0220312499979516));
#41296=CARTESIAN_POINT('',(-0.0219370137669058,0.0410227879449553,0.0221249999979516));
#41297=CARTESIAN_POINT('',(-0.025074456289703,0.0378853454221582,0.0222187499979516));
#41298=CARTESIAN_POINT('',(-0.0282118988125001,0.0347479028993611,0.0223124999979516));
#41299=CARTESIAN_POINT('',(-0.0282118988125,0.0303108891324553,0.0224062499979516));
#41300=CARTESIAN_POINT('',(-0.0282118988125001,0.0258738753655496,0.0224999999979516));
#41301=CARTESIAN_POINT('',(-0.025074456289703,0.0227364328427525,0.0225937499979516));
#41302=CARTESIAN_POINT('',(-0.0219370137669058,0.0195989903199553,0.0226874999979516));
#41303=CARTESIAN_POINT('',(-0.0175,0.0195989903199554,0.0227812499979516));
#41304=CARTESIAN_POINT('',(-0.0130629862330943,0.0195989903199553,0.0228749999979516));
#41305=CARTESIAN_POINT('',(-0.00992554371029717,0.0227364328427525,0.0229687499979516));
#41306=CARTESIAN_POINT('',(-0.00678810118750004,0.0258738753655496,0.0230624999979516));
#41307=CARTESIAN_POINT('',(-0.00678810118750004,0.0303108891324553,0.0231562499979516));
#41308=CARTESIAN_POINT('',(-0.00678810118750004,0.0347479028993611,0.0232499999979516));
#41309=CARTESIAN_POINT('',(-0.00992554371029717,0.0378853454221582,0.0233437499979516));
#41310=CARTESIAN_POINT('',(-0.0130629862330943,0.0410227879449553,0.0234374999979516));
#41311=CARTESIAN_POINT('',(-0.0175,0.0410227879449554,0.0235312499979516));
#41312=CARTESIAN_POINT('',(-0.0219370137669058,0.0410227879449553,0.0236249999979516));
#41313=CARTESIAN_POINT('',(-0.025074456289703,0.0378853454221582,0.0237187499979516));
#41314=CARTESIAN_POINT('',(-0.0282118988125001,0.0347479028993611,0.0238124999979516));
#41315=CARTESIAN_POINT('',(-0.0282118988125,0.0303108891324553,0.0239062499979516));
#41316=CARTESIAN_POINT('',(-0.0282118988125001,0.0258738753655496,0.0239999999979516));
#41317=CARTESIAN_POINT('',(-0.025074456289703,0.0227364328427525,0.0240937499979516));
#41318=CARTESIAN_POINT('',(-0.0219370137669058,0.0195989903199553,0.0241874999979516));
#41319=CARTESIAN_POINT('',(-0.0175,0.0195989903199554,0.0242812499979516));
#41320=CARTESIAN_POINT('',(-0.0130629862330943,0.0195989903199553,0.0243749999979516));
#41321=CARTESIAN_POINT('',(-0.00992554371029717,0.0227364328427525,0.0244687499979516));
#41322=CARTESIAN_POINT('',(-0.00678810118750004,0.0258738753655496,0.0245624999979516));
#41323=CARTESIAN_POINT('',(-0.00678810118750004,0.0303108891324553,0.0246562499979516));
#41324=CARTESIAN_POINT('',(-0.00678810118750004,0.0347479028993611,0.0247499999979516));
#41325=CARTESIAN_POINT('',(-0.00992554371029717,0.0378853454221582,0.0248437499979516));
#41326=CARTESIAN_POINT('',(-0.0130629862330943,0.0410227879449553,0.0249374999979516));
#41327=CARTESIAN_POINT('',(-0.0175,0.0410227879449554,0.0250312499979516));
#41328=CARTESIAN_POINT('',(-0.0219370137669058,0.0410227879449553,0.0251249999979516));
#41329=CARTESIAN_POINT('',(-0.025074456289703,0.0378853454221582,0.0252187499979516));
#41330=CARTESIAN_POINT('',(-0.0282118988125001,0.0347479028993611,0.0253124999979516));
#41331=CARTESIAN_POINT('',(-0.0282118988125,0.0303108891324553,0.0254062499979516));
#41332=CARTESIAN_POINT('',(-0.0282118988125001,0.0258738753655496,0.0254999999979516));
#41333=CARTESIAN_POINT('',(-0.025074456289703,0.0227364328427525,0.0255937499979516));
#41334=CARTESIAN_POINT('',(-0.0219370137669058,0.0195989903199553,0.0256874999979516));
#41335=CARTESIAN_POINT('',(-0.0175,0.0195989903199554,0.0257812499979516));
#41336=CARTESIAN_POINT('',(-0.0130629862330943,0.0195989903199553,0.0258749999979516));
#41337=CARTESIAN_POINT('',(-0.00992554371029717,0.0227364328427525,0.0259687499979516));
#41338=CARTESIAN_POINT('',(-0.00678810118750004,0.0258738753655496,0.0260624999979516));
#41339=CARTESIAN_POINT('',(-0.00678810118750004,0.0303108891324553,0.0261562499979516));
#41340=CARTESIAN_POINT('',(-0.00678810118750004,0.0347479028993611,0.0262499999979516));
#41341=CARTESIAN_POINT('',(-0.00992554371029717,0.0378853454221582,0.0263437499979516));
#41342=CARTESIAN_POINT('',(-0.0130629862330943,0.0410227879449553,0.0264374999979516));
#41343=CARTESIAN_POINT('',(-0.0175,0.0410227879449554,0.0265312499979516));
#41344=CARTESIAN_POINT('',(-0.0219370137669058,0.0410227879449553,0.0266249999979516));
#41345=CARTESIAN_POINT('',(-0.025074456289703,0.0378853454221582,0.0267187499979516));
#41346=CARTESIAN_POINT('',(-0.0282118988125001,0.0347479028993611,0.0268124999979516));
#41347=CARTESIAN_POINT('',(-0.0282118988125,0.0303108891324553,0.0269062499979516));
#41348=CARTESIAN_POINT('',(-0.0282118988125001,0.0258738753655496,0.0269999999979516));
#41349=CARTESIAN_POINT('',(-0.025074456289703,0.0227364328427525,0.0270937499979516));
#41350=CARTESIAN_POINT('',(-0.0219370137669058,0.0195989903199553,0.0271874999979516));
#41351=CARTESIAN_POINT('',(-0.0175,0.0195989903199554,0.0272812499979516));
#41352=CARTESIAN_POINT('',(-0.0130629862330943,0.0195989903199553,0.0273749999979516));
#41353=CARTESIAN_POINT('',(-0.00992554371029717,0.0227364328427525,0.0274687499979516));
#41354=CARTESIAN_POINT('',(-0.00678810118750004,0.0258738753655496,0.0275624999979516));
#41355=CARTESIAN_POINT('',(-0.00678810118750004,0.0303108891324553,0.0276562499979516));
#41356=CARTESIAN_POINT('',(-0.00678810118750004,0.0303108891324553,0.0276562499979516));
#41357=CARTESIAN_POINT('',(-0.00719405059375004,0.0303108891324553,0.0278906249969274));
#41358=CARTESIAN_POINT('',(-0.0076,0.0303108891324553,0.0281249999959032));
#41359=CARTESIAN_POINT('',(-0.0274,0.0303108891324553,0.0273749999959032));
#41360=CARTESIAN_POINT('',(-0.0274,0.0262101748649617,0.0274687499959032));
#41361=CARTESIAN_POINT('',(-0.0245003571337469,0.0233105319987085,0.0275624999959032));
#41362=CARTESIAN_POINT('',(-0.0216007142674937,0.0204108891324553,0.0276562499959032));
#41363=CARTESIAN_POINT('',(-0.0175,0.0204108891324553,0.0277499999959032));
#41364=CARTESIAN_POINT('',(-0.0133992857325064,0.0204108891324553,0.0278437499959032));
#41365=CARTESIAN_POINT('',(-0.0104996428662532,0.0233105319987085,0.0279374999959032));
#41366=CARTESIAN_POINT('',(-0.00760000000000004,0.0262101748649617,0.0280312499959032));
#41367=CARTESIAN_POINT('',(-0.0076,0.0303108891324553,0.0281249999959032));
#41368=CARTESIAN_POINT('',(-0.0274,0.0303108891324553,0.0273749999959032));
#41369=CARTESIAN_POINT('',(-0.0076,0.0303108891324553,0.0266249999959033));
#41370=CARTESIAN_POINT('',(-0.00760000000000004,0.0344116033999489,0.0267187499959032));
#41371=CARTESIAN_POINT('',(-0.0104996428662532,0.0373112462662021,0.0268124999959033));
#41372=CARTESIAN_POINT('',(-0.0133992857325064,0.0402108891324553,0.0269062499959032));
#41373=CARTESIAN_POINT('',(-0.0175,0.0402108891324554,0.0269999999959032));
#41374=CARTESIAN_POINT('',(-0.0216007142674937,0.0402108891324553,0.0270937499959032));
#41375=CARTESIAN_POINT('',(-0.0245003571337469,0.0373112462662021,0.0271874999959032));
#41376=CARTESIAN_POINT('',(-0.0274,0.0344116033999489,0.0272812499959032));
#41377=CARTESIAN_POINT('',(-0.0274,0.0303108891324553,0.0273749999959032));
#41378=CARTESIAN_POINT('',(-0.0076,0.0303108891324553,0.0266249999959033));
#41379=CARTESIAN_POINT('',(-0.0274,0.0303108891324553,0.0258749999959033));
#41380=CARTESIAN_POINT('',(-0.0274,0.0262101748649617,0.0259687499959032));
#41381=CARTESIAN_POINT('',(-0.0245003571337469,0.0233105319987085,0.0260624999959033));
#41382=CARTESIAN_POINT('',(-0.0216007142674937,0.0204108891324553,0.0261562499959032));
#41383=CARTESIAN_POINT('',(-0.0175,0.0204108891324553,0.0262499999959033));
#41384=CARTESIAN_POINT('',(-0.0133992857325064,0.0204108891324553,0.0263437499959032));
#41385=CARTESIAN_POINT('',(-0.0104996428662532,0.0233105319987085,0.0264374999959033));
#41386=CARTESIAN_POINT('',(-0.00760000000000004,0.0262101748649617,0.0265312499959032));
#41387=CARTESIAN_POINT('',(-0.0076,0.0303108891324553,0.0266249999959033));
#41388=CARTESIAN_POINT('',(-0.0274,0.0303108891324553,0.0258749999959033));
#41389=CARTESIAN_POINT('',(-0.0076,0.0303108891324553,0.0251249999959033));
#41390=CARTESIAN_POINT('',(-0.00760000000000002,0.034411603399949,0.0252187499959033));
#41391=CARTESIAN_POINT('',(-0.0104996428662532,0.0373112462662021,0.0253124999959033));
#41392=CARTESIAN_POINT('',(-0.0133992857325064,0.0402108891324553,0.0254062499959032));
#41393=CARTESIAN_POINT('',(-0.0175,0.0402108891324554,0.0254999999959033));
#41394=CARTESIAN_POINT('',(-0.0216007142674937,0.0402108891324553,0.0255937499959032));
#41395=CARTESIAN_POINT('',(-0.0245003571337469,0.0373112462662021,0.0256874999959033));
#41396=CARTESIAN_POINT('',(-0.0274,0.034411603399949,0.0257812499959032));
#41397=CARTESIAN_POINT('',(-0.0274,0.0303108891324553,0.0258749999959032));
#41398=CARTESIAN_POINT('',(-0.0076,0.0303108891324553,0.0251249999959033));
#41399=CARTESIAN_POINT('',(-0.0274,0.0303108891324553,0.0243749999959033));
#41400=CARTESIAN_POINT('',(-0.0274000000000001,0.0262101748649617,0.0244687499959032));
#41401=CARTESIAN_POINT('',(-0.0245003571337469,0.0233105319987085,0.0245624999959033));
#41402=CARTESIAN_POINT('',(-0.0216007142674937,0.0204108891324553,0.0246562499959032));
#41403=CARTESIAN_POINT('',(-0.0175,0.0204108891324553,0.0247499999959033));
#41404=CARTESIAN_POINT('',(-0.0133992857325064,0.0204108891324553,0.0248437499959032));
#41405=CARTESIAN_POINT('',(-0.0104996428662532,0.0233105319987085,0.0249374999959033));
#41406=CARTESIAN_POINT('',(-0.00760000000000006,0.0262101748649616,0.0250312499959033));
#41407=CARTESIAN_POINT('',(-0.0076,0.0303108891324553,0.0251249999959032));
#41408=CARTESIAN_POINT('',(-0.0274,0.0303108891324553,0.0243749999959032));
#41409=CARTESIAN_POINT('',(-0.0076,0.0303108891324553,0.0236249999959032));
#41410=CARTESIAN_POINT('',(-0.00760000000000006,0.034411603399949,0.0237187499959032));
#41411=CARTESIAN_POINT('',(-0.0104996428662532,0.0373112462662021,0.0238124999959032));
#41412=CARTESIAN_POINT('',(-0.0133992857325064,0.0402108891324553,0.0239062499959032));
#41413=CARTESIAN_POINT('',(-0.0175,0.0402108891324554,0.0239999999959032));
#41414=CARTESIAN_POINT('',(-0.0216007142674937,0.0402108891324553,0.0240937499959032));
#41415=CARTESIAN_POINT('',(-0.0245003571337469,0.0373112462662021,0.0241874999959032));
#41416=CARTESIAN_POINT('',(-0.0274,0.034411603399949,0.0242812499959032));
#41417=CARTESIAN_POINT('',(-0.0274,0.0303108891324553,0.0243749999959032));
#41418=CARTESIAN_POINT('',(-0.0076,0.0303108891324553,0.0236249999959032));
#41419=CARTESIAN_POINT('',(-0.0274,0.0303108891324553,0.0228749999959032));
#41420=CARTESIAN_POINT('',(-0.0274,0.0262101748649617,0.0229687499959032));
#41421=CARTESIAN_POINT('',(-0.0245003571337469,0.0233105319987085,0.0230624999959032));
#41422=CARTESIAN_POINT('',(-0.0216007142674937,0.0204108891324553,0.0231562499959032));
#41423=CARTESIAN_POINT('',(-0.0175,0.0204108891324553,0.0232499999959032));
#41424=CARTESIAN_POINT('',(-0.0133992857325064,0.0204108891324553,0.0233437499959032));
#41425=CARTESIAN_POINT('',(-0.0104996428662532,0.0233105319987085,0.0234374999959032));
#41426=CARTESIAN_POINT('',(-0.00760000000000003,0.0262101748649617,0.0235312499959033));
#41427=CARTESIAN_POINT('',(-0.0076,0.0303108891324553,0.0236249999959032));
#41428=CARTESIAN_POINT('',(-0.0274,0.0303108891324553,0.0228749999959033));
#41429=CARTESIAN_POINT('',(-0.0076,0.0303108891324553,0.0221249999959033));
#41430=CARTESIAN_POINT('',(-0.00760000000000004,0.0344116033999489,0.0222187499959032));
#41431=CARTESIAN_POINT('',(-0.0104996428662532,0.0373112462662021,0.0223124999959033));
#41432=CARTESIAN_POINT('',(-0.0133992857325064,0.0402108891324553,0.0224062499959032));
#41433=CARTESIAN_POINT('',(-0.0175,0.0402108891324554,0.0224999999959033));
#41434=CARTESIAN_POINT('',(-0.0216007142674937,0.0402108891324553,0.0225937499959032));
#41435=CARTESIAN_POINT('',(-0.0245003571337469,0.0373112462662021,0.0226874999959033));
#41436=CARTESIAN_POINT('',(-0.0274,0.0344116033999489,0.0227812499959032));
#41437=CARTESIAN_POINT('',(-0.0274,0.0303108891324553,0.0228749999959033));
#41438=CARTESIAN_POINT('',(-0.0076,0.0303108891324553,0.021));
#41439=CARTESIAN_POINT('',(-0.00760000000000004,0.0344116033999489,0.02109375));
#41440=CARTESIAN_POINT('',(-0.0104996428662532,0.0373112462662021,0.0211875));
#41441=CARTESIAN_POINT('',(-0.0133992857325064,0.0402108891324553,0.02128125));
#41442=CARTESIAN_POINT('',(-0.0175,0.0402108891324554,0.021375));
#41443=CARTESIAN_POINT('',(-0.0216007142674937,0.0402108891324553,0.02146875));
#41444=CARTESIAN_POINT('',(-0.0245003571337469,0.0373112462662021,0.0215625));
#41445=CARTESIAN_POINT('',(-0.0274,0.0344116033999489,0.02165625));
#41446=CARTESIAN_POINT('',(-0.0274,0.0303108891324553,0.02175));
#41447=CARTESIAN_POINT('',(-0.0274,0.0262101748649617,0.02184375));
#41448=CARTESIAN_POINT('',(-0.0245003571337469,0.0233105319987085,0.0219375));
#41449=CARTESIAN_POINT('',(-0.0216007142674937,0.0204108891324553,0.02203125));
#41450=CARTESIAN_POINT('',(-0.0175,0.0204108891324553,0.022125));
#41451=CARTESIAN_POINT('',(-0.0133992857325064,0.0204108891324553,0.02221875));
#41452=CARTESIAN_POINT('',(-0.0104996428662532,0.0233105319987085,0.0223125));
#41453=CARTESIAN_POINT('',(-0.00760000000000004,0.0262101748649617,0.02240625));
#41454=CARTESIAN_POINT('',(-0.0076,0.0303108891324553,0.0225));
#41455=CARTESIAN_POINT('',(-0.00760000000000004,0.0344116033999489,0.02259375));
#41456=CARTESIAN_POINT('',(-0.0104996428662532,0.0373112462662021,0.0226875));
#41457=CARTESIAN_POINT('',(-0.0133992857325064,0.0402108891324553,0.02278125));
#41458=CARTESIAN_POINT('',(-0.0175,0.0402108891324554,0.022875));
#41459=CARTESIAN_POINT('',(-0.0216007142674937,0.0402108891324553,0.02296875));
#41460=CARTESIAN_POINT('',(-0.0245003571337469,0.0373112462662021,0.0230625));
#41461=CARTESIAN_POINT('',(-0.0274,0.0344116033999489,0.02315625));
#41462=CARTESIAN_POINT('',(-0.0274,0.0303108891324553,0.02325));
#41463=CARTESIAN_POINT('',(-0.0274,0.0262101748649617,0.02334375));
#41464=CARTESIAN_POINT('',(-0.0245003571337469,0.0233105319987085,0.0234375));
#41465=CARTESIAN_POINT('',(-0.0216007142674937,0.0204108891324553,0.02353125));
#41466=CARTESIAN_POINT('',(-0.0175,0.0204108891324553,0.023625));
#41467=CARTESIAN_POINT('',(-0.0133992857325064,0.0204108891324553,0.02371875));
#41468=CARTESIAN_POINT('',(-0.0104996428662532,0.0233105319987085,0.0238125));
#41469=CARTESIAN_POINT('',(-0.00760000000000004,0.0262101748649617,0.02390625));
#41470=CARTESIAN_POINT('',(-0.0076,0.0303108891324553,0.024));
#41471=CARTESIAN_POINT('',(-0.00760000000000004,0.0344116033999489,0.02409375));
#41472=CARTESIAN_POINT('',(-0.0104996428662532,0.0373112462662021,0.0241875));
#41473=CARTESIAN_POINT('',(-0.0133992857325064,0.0402108891324553,0.02428125));
#41474=CARTESIAN_POINT('',(-0.0175,0.0402108891324554,0.024375));
#41475=CARTESIAN_POINT('',(-0.0216007142674937,0.0402108891324553,0.02446875));
#41476=CARTESIAN_POINT('',(-0.0245003571337469,0.0373112462662021,0.0245625));
#41477=CARTESIAN_POINT('',(-0.0274,0.0344116033999489,0.02465625));
#41478=CARTESIAN_POINT('',(-0.0274,0.0303108891324553,0.02475));
#41479=CARTESIAN_POINT('',(-0.0274,0.0262101748649617,0.02484375));
#41480=CARTESIAN_POINT('',(-0.0245003571337469,0.0233105319987085,0.0249375));
#41481=CARTESIAN_POINT('',(-0.0216007142674937,0.0204108891324553,0.02503125));
#41482=CARTESIAN_POINT('',(-0.0175,0.0204108891324553,0.025125));
#41483=CARTESIAN_POINT('',(-0.0133992857325064,0.0204108891324553,0.02521875));
#41484=CARTESIAN_POINT('',(-0.0104996428662532,0.0233105319987085,0.0253125));
#41485=CARTESIAN_POINT('',(-0.00760000000000004,0.0262101748649617,0.02540625));
#41486=CARTESIAN_POINT('',(-0.0076,0.0303108891324553,0.0255));
#41487=CARTESIAN_POINT('',(-0.00760000000000004,0.0344116033999489,0.02559375));
#41488=CARTESIAN_POINT('',(-0.0104996428662532,0.0373112462662021,0.0256875));
#41489=CARTESIAN_POINT('',(-0.0133992857325064,0.0402108891324553,0.02578125));
#41490=CARTESIAN_POINT('',(-0.0175,0.0402108891324554,0.025875));
#41491=CARTESIAN_POINT('',(-0.0216007142674937,0.0402108891324553,0.02596875));
#41492=CARTESIAN_POINT('',(-0.0245003571337469,0.0373112462662021,0.0260625));
#41493=CARTESIAN_POINT('',(-0.0274,0.0344116033999489,0.02615625));
#41494=CARTESIAN_POINT('',(-0.0274,0.0303108891324553,0.02625));
#41495=CARTESIAN_POINT('',(-0.0274,0.0262101748649617,0.02634375));
#41496=CARTESIAN_POINT('',(-0.0245003571337469,0.0233105319987085,0.0264375));
#41497=CARTESIAN_POINT('',(-0.0216007142674937,0.0204108891324553,0.02653125));
#41498=CARTESIAN_POINT('',(-0.0175,0.0204108891324553,0.026625));
#41499=CARTESIAN_POINT('',(-0.0133992857325064,0.0204108891324553,0.02671875));
#41500=CARTESIAN_POINT('',(-0.0104996428662532,0.0233105319987085,0.0268125));
#41501=CARTESIAN_POINT('',(-0.00760000000000004,0.0262101748649617,0.02690625));
#41502=CARTESIAN_POINT('',(-0.0076,0.0303108891324553,0.027));
#41503=CARTESIAN_POINT('',(-0.00678810118750004,0.0303108891324553,0.0214687499979516));
#41504=CARTESIAN_POINT('',(-0.00678810118750004,0.0347479028993611,0.0215624999979516));
#41505=CARTESIAN_POINT('',(-0.00992554371029717,0.0378853454221582,0.0216562499979516));
#41506=CARTESIAN_POINT('',(-0.0130629862330943,0.0410227879449553,0.0217499999979516));
#41507=CARTESIAN_POINT('',(-0.0175,0.0410227879449554,0.0218437499979516));
#41508=CARTESIAN_POINT('',(-0.0219370137669058,0.0410227879449553,0.0219374999979516));
#41509=CARTESIAN_POINT('',(-0.025074456289703,0.0378853454221582,0.0220312499979516));
#41510=CARTESIAN_POINT('',(-0.0282118988125001,0.0347479028993611,0.0221249999979516));
#41511=CARTESIAN_POINT('',(-0.0282118988125,0.0303108891324553,0.0222187499979516));
#41512=CARTESIAN_POINT('',(-0.0282118988125001,0.0258738753655496,0.0223124999979516));
#41513=CARTESIAN_POINT('',(-0.025074456289703,0.0227364328427525,0.0224062499979516));
#41514=CARTESIAN_POINT('',(-0.0219370137669058,0.0195989903199553,0.0224999999979516));
#41515=CARTESIAN_POINT('',(-0.0175,0.0195989903199554,0.0225937499979516));
#41516=CARTESIAN_POINT('',(-0.0130629862330943,0.0195989903199553,0.0226874999979516));
#41517=CARTESIAN_POINT('',(-0.00992554371029717,0.0227364328427525,0.0227812499979516));
#41518=CARTESIAN_POINT('',(-0.00678810118750004,0.0258738753655496,0.0228749999979516));
#41519=CARTESIAN_POINT('',(-0.00678810118750004,0.0303108891324553,0.0229687499979516));
#41520=CARTESIAN_POINT('',(-0.00678810118750004,0.0347479028993611,0.0230624999979516));
#41521=CARTESIAN_POINT('',(-0.00992554371029717,0.0378853454221582,0.0231562499979516));
#41522=CARTESIAN_POINT('',(-0.0130629862330943,0.0410227879449553,0.0232499999979516));
#41523=CARTESIAN_POINT('',(-0.0175,0.0410227879449554,0.0233437499979516));
#41524=CARTESIAN_POINT('',(-0.0219370137669058,0.0410227879449553,0.0234374999979516));
#41525=CARTESIAN_POINT('',(-0.025074456289703,0.0378853454221582,0.0235312499979516));
#41526=CARTESIAN_POINT('',(-0.0282118988125001,0.0347479028993611,0.0236249999979516));
#41527=CARTESIAN_POINT('',(-0.0282118988125,0.0303108891324553,0.0237187499979516));
#41528=CARTESIAN_POINT('',(-0.0282118988125001,0.0258738753655496,0.0238124999979516));
#41529=CARTESIAN_POINT('',(-0.025074456289703,0.0227364328427525,0.0239062499979516));
#41530=CARTESIAN_POINT('',(-0.0219370137669058,0.0195989903199553,0.0239999999979516));
#41531=CARTESIAN_POINT('',(-0.0175,0.0195989903199554,0.0240937499979516));
#41532=CARTESIAN_POINT('',(-0.0130629862330943,0.0195989903199553,0.0241874999979516));
#41533=CARTESIAN_POINT('',(-0.00992554371029717,0.0227364328427525,0.0242812499979516));
#41534=CARTESIAN_POINT('',(-0.00678810118750004,0.0258738753655496,0.0243749999979516));
#41535=CARTESIAN_POINT('',(-0.00678810118750004,0.0303108891324553,0.0244687499979516));
#41536=CARTESIAN_POINT('',(-0.00678810118750004,0.0347479028993611,0.0245624999979516));
#41537=CARTESIAN_POINT('',(-0.00992554371029717,0.0378853454221582,0.0246562499979516));
#41538=CARTESIAN_POINT('',(-0.0130629862330943,0.0410227879449553,0.0247499999979516));
#41539=CARTESIAN_POINT('',(-0.0175,0.0410227879449554,0.0248437499979516));
#41540=CARTESIAN_POINT('',(-0.0219370137669058,0.0410227879449553,0.0249374999979516));
#41541=CARTESIAN_POINT('',(-0.025074456289703,0.0378853454221582,0.0250312499979516));
#41542=CARTESIAN_POINT('',(-0.0282118988125001,0.0347479028993611,0.0251249999979516));
#41543=CARTESIAN_POINT('',(-0.0282118988125,0.0303108891324553,0.0252187499979516));
#41544=CARTESIAN_POINT('',(-0.0282118988125001,0.0258738753655496,0.0253124999979516));
#41545=CARTESIAN_POINT('',(-0.025074456289703,0.0227364328427525,0.0254062499979516));
#41546=CARTESIAN_POINT('',(-0.0219370137669058,0.0195989903199553,0.0254999999979516));
#41547=CARTESIAN_POINT('',(-0.0175,0.0195989903199554,0.0255937499979516));
#41548=CARTESIAN_POINT('',(-0.0130629862330943,0.0195989903199553,0.0256874999979516));
#41549=CARTESIAN_POINT('',(-0.00992554371029717,0.0227364328427525,0.0257812499979516));
#41550=CARTESIAN_POINT('',(-0.00678810118750004,0.0258738753655496,0.0258749999979516));
#41551=CARTESIAN_POINT('',(-0.00678810118750004,0.0303108891324553,0.0259687499979516));
#41552=CARTESIAN_POINT('',(-0.00678810118750004,0.0347479028993611,0.0260624999979516));
#41553=CARTESIAN_POINT('',(-0.00992554371029717,0.0378853454221582,0.0261562499979516));
#41554=CARTESIAN_POINT('',(-0.0130629862330943,0.0410227879449553,0.0262499999979516));
#41555=CARTESIAN_POINT('',(-0.0175,0.0410227879449554,0.0263437499979516));
#41556=CARTESIAN_POINT('',(-0.0219370137669058,0.0410227879449553,0.0264374999979516));
#41557=CARTESIAN_POINT('',(-0.025074456289703,0.0378853454221582,0.0265312499979516));
#41558=CARTESIAN_POINT('',(-0.0282118988125001,0.0347479028993611,0.0266249999979516));
#41559=CARTESIAN_POINT('',(-0.0282118988125,0.0303108891324553,0.0267187499979516));
#41560=CARTESIAN_POINT('',(-0.0282118988125001,0.0258738753655496,0.0268124999979516));
#41561=CARTESIAN_POINT('',(-0.025074456289703,0.0227364328427525,0.0269062499979516));
#41562=CARTESIAN_POINT('',(-0.0219370137669058,0.0195989903199553,0.0269999999979516));
#41563=CARTESIAN_POINT('',(-0.0175,0.0195989903199554,0.0270937499979516));
#41564=CARTESIAN_POINT('',(-0.0130629862330943,0.0195989903199553,0.0271874999979516));
#41565=CARTESIAN_POINT('',(-0.00992554371029717,0.0227364328427525,0.0272812499979516));
#41566=CARTESIAN_POINT('',(-0.00678810118750004,0.0258738753655496,0.0273749999979516));
#41567=CARTESIAN_POINT('',(-0.00678810118750004,0.0303108891324553,0.0274687499979516));
#41568=CARTESIAN_POINT('',(-0.00719405059375004,0.0303108891324553,0.0212343749989758));
#41569=CARTESIAN_POINT('',(-0.0076,0.0303108891324553,0.021));
#41570=CARTESIAN_POINT('',(-0.00678810118750004,0.0303108891324553,0.0214687499979516));
#41571=CARTESIAN_POINT('',(-0.0076,0.0303108891324553,0.021));
#41572=CARTESIAN_POINT('',(-0.00760000000000004,0.0344116033999489,0.02109375));
#41573=CARTESIAN_POINT('',(-0.0104996428662532,0.0373112462662021,0.0211875));
#41574=CARTESIAN_POINT('',(-0.0133992857325064,0.0402108891324553,0.02128125));
#41575=CARTESIAN_POINT('',(-0.0175,0.0402108891324554,0.021375));
#41576=CARTESIAN_POINT('',(-0.0216007142674937,0.0402108891324553,0.02146875));
#41577=CARTESIAN_POINT('',(-0.0245003571337469,0.0373112462662021,0.0215625));
#41578=CARTESIAN_POINT('',(-0.0274,0.0344116033999489,0.02165625));
#41579=CARTESIAN_POINT('',(-0.0274,0.0303108891324553,0.02175));
#41580=CARTESIAN_POINT('',(-0.0274,0.0303108891324553,0.02175));
#41581=CARTESIAN_POINT('',(-0.0274,0.0303108891324553,0.02175));
#41582=CARTESIAN_POINT('',(-0.0274,0.0262101748649617,0.02184375));
#41583=CARTESIAN_POINT('',(-0.0245003571337469,0.0233105319987085,0.0219375));
#41584=CARTESIAN_POINT('',(-0.0216007142674937,0.0204108891324553,0.02203125));
#41585=CARTESIAN_POINT('',(-0.0175,0.0204108891324553,0.022125));
#41586=CARTESIAN_POINT('',(-0.0133992857325064,0.0204108891324553,0.02221875));
#41587=CARTESIAN_POINT('',(-0.0104996428662532,0.0233105319987085,0.0223125));
#41588=CARTESIAN_POINT('',(-0.00760000000000003,0.0262101748649617,0.02240625));
#41589=CARTESIAN_POINT('',(-0.0076,0.0303108891324553,0.0225));
#41590=CARTESIAN_POINT('',(-0.0076,0.0303108891324553,0.0225));
#41591=CARTESIAN_POINT('',(-0.0076,0.0303108891324553,0.0225));
#41592=CARTESIAN_POINT('',(-0.00760000000000006,0.034411603399949,0.02259375));
#41593=CARTESIAN_POINT('',(-0.0104996428662532,0.0373112462662021,0.0226875));
#41594=CARTESIAN_POINT('',(-0.0133992857325064,0.0402108891324553,0.02278125));
#41595=CARTESIAN_POINT('',(-0.0175,0.0402108891324554,0.022875));
#41596=CARTESIAN_POINT('',(-0.0216007142674937,0.0402108891324553,0.02296875));
#41597=CARTESIAN_POINT('',(-0.0245003571337469,0.0373112462662021,0.0230625));
#41598=CARTESIAN_POINT('',(-0.0274000000000001,0.0344116033999489,0.02315625));
#41599=CARTESIAN_POINT('',(-0.0274,0.0303108891324553,0.02325));
#41600=CARTESIAN_POINT('',(-0.0274,0.0303108891324553,0.02325));
#41601=CARTESIAN_POINT('',(-0.0274,0.0303108891324553,0.02325));
#41602=CARTESIAN_POINT('',(-0.0274,0.0262101748649617,0.02334375));
#41603=CARTESIAN_POINT('',(-0.0245003571337469,0.0233105319987085,0.0234375));
#41604=CARTESIAN_POINT('',(-0.0216007142674937,0.0204108891324553,0.02353125));
#41605=CARTESIAN_POINT('',(-0.0175,0.0204108891324553,0.023625));
#41606=CARTESIAN_POINT('',(-0.0133992857325064,0.0204108891324553,0.02371875));
#41607=CARTESIAN_POINT('',(-0.0104996428662532,0.0233105319987085,0.0238125));
#41608=CARTESIAN_POINT('',(-0.00760000000000006,0.0262101748649616,0.02390625));
#41609=CARTESIAN_POINT('',(-0.0076,0.0303108891324553,0.024));
#41610=CARTESIAN_POINT('',(-0.0076,0.0303108891324553,0.024));
#41611=CARTESIAN_POINT('',(-0.0076,0.0303108891324553,0.024));
#41612=CARTESIAN_POINT('',(-0.00760000000000002,0.034411603399949,0.02409375));
#41613=CARTESIAN_POINT('',(-0.0104996428662532,0.0373112462662021,0.0241875));
#41614=CARTESIAN_POINT('',(-0.0133992857325064,0.0402108891324553,0.02428125));
#41615=CARTESIAN_POINT('',(-0.0175,0.0402108891324554,0.024375));
#41616=CARTESIAN_POINT('',(-0.0216007142674937,0.0402108891324553,0.02446875));
#41617=CARTESIAN_POINT('',(-0.0245003571337469,0.0373112462662021,0.0245625));
#41618=CARTESIAN_POINT('',(-0.0274,0.034411603399949,0.02465625));
#41619=CARTESIAN_POINT('',(-0.0274,0.0303108891324553,0.02475));
#41620=CARTESIAN_POINT('',(-0.0274,0.0303108891324553,0.02475));
#41621=CARTESIAN_POINT('',(-0.0274,0.0303108891324553,0.02475));
#41622=CARTESIAN_POINT('',(-0.0274,0.0262101748649617,0.02484375));
#41623=CARTESIAN_POINT('',(-0.0245003571337469,0.0233105319987085,0.0249375));
#41624=CARTESIAN_POINT('',(-0.0216007142674937,0.0204108891324553,0.02503125));
#41625=CARTESIAN_POINT('',(-0.0175,0.0204108891324553,0.025125));
#41626=CARTESIAN_POINT('',(-0.0133992857325064,0.0204108891324553,0.02521875));
#41627=CARTESIAN_POINT('',(-0.0104996428662532,0.0233105319987085,0.0253125));
#41628=CARTESIAN_POINT('',(-0.00760000000000004,0.0262101748649617,0.02540625));
#41629=CARTESIAN_POINT('',(-0.0076,0.0303108891324553,0.0255));
#41630=CARTESIAN_POINT('',(-0.0076,0.0303108891324553,0.0255));
#41631=CARTESIAN_POINT('',(-0.0076,0.0303108891324553,0.0255));
#41632=CARTESIAN_POINT('',(-0.00760000000000004,0.0344116033999489,0.02559375));
#41633=CARTESIAN_POINT('',(-0.0104996428662532,0.0373112462662021,0.0256875));
#41634=CARTESIAN_POINT('',(-0.0133992857325064,0.0402108891324553,0.02578125));
#41635=CARTESIAN_POINT('',(-0.0175,0.0402108891324554,0.025875));
#41636=CARTESIAN_POINT('',(-0.0216007142674937,0.0402108891324553,0.02596875));
#41637=CARTESIAN_POINT('',(-0.0245003571337469,0.0373112462662021,0.0260625));
#41638=CARTESIAN_POINT('',(-0.0274,0.0344116033999489,0.02615625));
#41639=CARTESIAN_POINT('',(-0.0274,0.0303108891324553,0.02625));
#41640=CARTESIAN_POINT('',(-0.0274,0.0303108891324553,0.02625));
#41641=CARTESIAN_POINT('',(-0.0274,0.0303108891324553,0.02625));
#41642=CARTESIAN_POINT('',(-0.0274,0.0262101748649617,0.02634375));
#41643=CARTESIAN_POINT('',(-0.0245003571337469,0.0233105319987085,0.0264375));
#41644=CARTESIAN_POINT('',(-0.0216007142674937,0.0204108891324553,0.02653125));
#41645=CARTESIAN_POINT('',(-0.0175,0.0204108891324553,0.026625));
#41646=CARTESIAN_POINT('',(-0.0133992857325064,0.0204108891324553,0.02671875));
#41647=CARTESIAN_POINT('',(-0.0104996428662532,0.0233105319987085,0.0268125));
#41648=CARTESIAN_POINT('',(-0.00760000000000004,0.0262101748649617,0.02690625));
#41649=CARTESIAN_POINT('',(-0.0076,0.0303108891324553,0.027));
#41650=CARTESIAN_POINT('',(-0.0076,0.0303108891324553,0.027));
#41651=CARTESIAN_POINT('',(-0.00719405059375004,0.0303108891324553,0.0272343749989758));
#41652=CARTESIAN_POINT('',(-0.00678810118750004,0.0303108891324553,0.0274687499979516));
#41653=CARTESIAN_POINT('',(-0.00678810118750004,0.0303108891324553,0.0214687499979516));
#41654=CARTESIAN_POINT('',(-0.00678810118750004,0.0347479028993611,0.0215624999979516));
#41655=CARTESIAN_POINT('',(-0.00992554371029717,0.0378853454221582,0.0216562499979516));
#41656=CARTESIAN_POINT('',(-0.0130629862330943,0.0410227879449553,0.0217499999979516));
#41657=CARTESIAN_POINT('',(-0.0175,0.0410227879449554,0.0218437499979516));
#41658=CARTESIAN_POINT('',(-0.0219370137669058,0.0410227879449553,0.0219374999979516));
#41659=CARTESIAN_POINT('',(-0.025074456289703,0.0378853454221582,0.0220312499979516));
#41660=CARTESIAN_POINT('',(-0.0282118988125001,0.0347479028993611,0.0221249999979516));
#41661=CARTESIAN_POINT('',(-0.0282118988125,0.0303108891324553,0.0222187499979516));
#41662=CARTESIAN_POINT('',(-0.0282118988125001,0.0258738753655496,0.0223124999979516));
#41663=CARTESIAN_POINT('',(-0.025074456289703,0.0227364328427525,0.0224062499979516));
#41664=CARTESIAN_POINT('',(-0.0219370137669058,0.0195989903199553,0.0224999999979516));
#41665=CARTESIAN_POINT('',(-0.0175,0.0195989903199554,0.0225937499979516));
#41666=CARTESIAN_POINT('',(-0.0130629862330943,0.0195989903199553,0.0226874999979516));
#41667=CARTESIAN_POINT('',(-0.00992554371029717,0.0227364328427525,0.0227812499979516));
#41668=CARTESIAN_POINT('',(-0.00678810118750004,0.0258738753655496,0.0228749999979516));
#41669=CARTESIAN_POINT('',(-0.00678810118750004,0.0303108891324553,0.0229687499979516));
#41670=CARTESIAN_POINT('',(-0.00678810118750004,0.0347479028993611,0.0230624999979516));
#41671=CARTESIAN_POINT('',(-0.00992554371029717,0.0378853454221582,0.0231562499979516));
#41672=CARTESIAN_POINT('',(-0.0130629862330943,0.0410227879449553,0.0232499999979516));
#41673=CARTESIAN_POINT('',(-0.0175,0.0410227879449554,0.0233437499979516));
#41674=CARTESIAN_POINT('',(-0.0219370137669058,0.0410227879449553,0.0234374999979516));
#41675=CARTESIAN_POINT('',(-0.025074456289703,0.0378853454221582,0.0235312499979516));
#41676=CARTESIAN_POINT('',(-0.0282118988125001,0.0347479028993611,0.0236249999979516));
#41677=CARTESIAN_POINT('',(-0.0282118988125,0.0303108891324553,0.0237187499979516));
#41678=CARTESIAN_POINT('',(-0.0282118988125001,0.0258738753655496,0.0238124999979516));
#41679=CARTESIAN_POINT('',(-0.025074456289703,0.0227364328427525,0.0239062499979516));
#41680=CARTESIAN_POINT('',(-0.0219370137669058,0.0195989903199553,0.0239999999979516));
#41681=CARTESIAN_POINT('',(-0.0175,0.0195989903199554,0.0240937499979516));
#41682=CARTESIAN_POINT('',(-0.0130629862330943,0.0195989903199553,0.0241874999979516));
#41683=CARTESIAN_POINT('',(-0.00992554371029717,0.0227364328427525,0.0242812499979516));
#41684=CARTESIAN_POINT('',(-0.00678810118750004,0.0258738753655496,0.0243749999979516));
#41685=CARTESIAN_POINT('',(-0.00678810118750004,0.0303108891324553,0.0244687499979516));
#41686=CARTESIAN_POINT('',(-0.00678810118750004,0.0347479028993611,0.0245624999979516));
#41687=CARTESIAN_POINT('',(-0.00992554371029717,0.0378853454221582,0.0246562499979516));
#41688=CARTESIAN_POINT('',(-0.0130629862330943,0.0410227879449553,0.0247499999979516));
#41689=CARTESIAN_POINT('',(-0.0175,0.0410227879449554,0.0248437499979516));
#41690=CARTESIAN_POINT('',(-0.0219370137669058,0.0410227879449553,0.0249374999979516));
#41691=CARTESIAN_POINT('',(-0.025074456289703,0.0378853454221582,0.0250312499979516));
#41692=CARTESIAN_POINT('',(-0.0282118988125001,0.0347479028993611,0.0251249999979516));
#41693=CARTESIAN_POINT('',(-0.0282118988125,0.0303108891324553,0.0252187499979516));
#41694=CARTESIAN_POINT('',(-0.0282118988125001,0.0258738753655496,0.0253124999979516));
#41695=CARTESIAN_POINT('',(-0.025074456289703,0.0227364328427525,0.0254062499979516));
#41696=CARTESIAN_POINT('',(-0.0219370137669058,0.0195989903199553,0.0254999999979516));
#41697=CARTESIAN_POINT('',(-0.0175,0.0195989903199554,0.0255937499979516));
#41698=CARTESIAN_POINT('',(-0.0130629862330943,0.0195989903199553,0.0256874999979516));
#41699=CARTESIAN_POINT('',(-0.00992554371029717,0.0227364328427525,0.0257812499979516));
#41700=CARTESIAN_POINT('',(-0.00678810118750004,0.0258738753655496,0.0258749999979516));
#41701=CARTESIAN_POINT('',(-0.00678810118750004,0.0303108891324553,0.0259687499979516));
#41702=CARTESIAN_POINT('',(-0.00678810118750004,0.0347479028993611,0.0260624999979516));
#41703=CARTESIAN_POINT('',(-0.00992554371029717,0.0378853454221582,0.0261562499979516));
#41704=CARTESIAN_POINT('',(-0.0130629862330943,0.0410227879449553,0.0262499999979516));
#41705=CARTESIAN_POINT('',(-0.0175,0.0410227879449554,0.0263437499979516));
#41706=CARTESIAN_POINT('',(-0.0219370137669058,0.0410227879449553,0.0264374999979516));
#41707=CARTESIAN_POINT('',(-0.025074456289703,0.0378853454221582,0.0265312499979516));
#41708=CARTESIAN_POINT('',(-0.0282118988125001,0.0347479028993611,0.0266249999979516));
#41709=CARTESIAN_POINT('',(-0.0282118988125,0.0303108891324553,0.0267187499979516));
#41710=CARTESIAN_POINT('',(-0.0282118988125001,0.0258738753655496,0.0268124999979516));
#41711=CARTESIAN_POINT('',(-0.025074456289703,0.0227364328427525,0.0269062499979516));
#41712=CARTESIAN_POINT('',(-0.0219370137669058,0.0195989903199553,0.0269999999979516));
#41713=CARTESIAN_POINT('',(-0.0175,0.0195989903199554,0.0270937499979516));
#41714=CARTESIAN_POINT('',(-0.0130629862330943,0.0195989903199553,0.0271874999979516));
#41715=CARTESIAN_POINT('',(-0.00992554371029717,0.0227364328427525,0.0272812499979516));
#41716=CARTESIAN_POINT('',(-0.00678810118750004,0.0258738753655496,0.0273749999979516));
#41717=CARTESIAN_POINT('',(-0.00678810118750004,0.0303108891324553,0.0274687499979516));
#41718=CARTESIAN_POINT('',(-0.0175,0.0303108891324553,0.0227055389329771));
#41719=CARTESIAN_POINT('',(-0.00678810118750004,0.0303108891324553,0.0215624999979516));
#41720=CARTESIAN_POINT('',(-0.00678810118750004,0.0303108891324553,0.0275624999979516));
#41721=CARTESIAN_POINT('',(-0.00678810118750004,0.0303108891324553,0.0275624999979516));
#41722=CARTESIAN_POINT('',(-0.0076,0.0303108891324553,0.0275624999979516));
#41723=CARTESIAN_POINT('',(-0.00678810118750004,0.0303108891324553,0.0275624999979516));
#41724=CARTESIAN_POINT('',(-0.0076,0.0303108891324553,0.0215624999979516));
#41725=CARTESIAN_POINT('',(-0.0115,0.0303108891324553,0.031));
#41726=CARTESIAN_POINT('',(-0.00953134086570699,0.0310183293076278,0.021011430723831));
#41727=CARTESIAN_POINT('',(-0.00953134086570699,0.0310183293076278,0.021));
#41728=CARTESIAN_POINT('',(-0.00953134086570699,0.0310183293076278,0.026));
#41729=CARTESIAN_POINT('',(-0.0115,0.0303108891324553,0.026));
#41730=CARTESIAN_POINT('',(-0.00953134086570699,0.0296034489572829,0.026));
#41731=CARTESIAN_POINT('',(-0.00953134086570699,0.0296034489572829,0.021011430723831));
#41732=CARTESIAN_POINT('',(-0.00953134086570699,0.0296034489572829,0.021));
#41733=CARTESIAN_POINT('',(-0.0115,0.0303108891324553,0.021));
#41734=CARTESIAN_POINT('',(-0.0115,0.0303108891324553,0.031));
#41735=CARTESIAN_POINT('',(-0.0115,0.0303108891324553,0.031));
#41736=CARTESIAN_POINT('',(-0.013,0.0303108891324553,0.031));
#41737=CARTESIAN_POINT('',(-0.0115,0.0303108891324553,0.031));
#41738=CARTESIAN_POINT('',(-0.0105,0.0303108891324553,0.031));
#41739=CARTESIAN_POINT('',(-0.0175,0.0303108891324553,0.014));
#41740=CARTESIAN_POINT('',(-0.0101875,0.027066302294351,0.026));
#41741=CARTESIAN_POINT('',(-0.0101875,0.027066302294351,0.021));
#41742=CARTESIAN_POINT('',(-0.0175,0.0303108891324553,0.021));
#41743=CARTESIAN_POINT('',(-0.0101875,0.0335554759705597,0.021));
#41744=CARTESIAN_POINT('',(-0.0101875,0.0335554759705597,0.026));
#41745=CARTESIAN_POINT('',(-0.0099006579232147,0.0328108891324553,0.0142731879764631));
#41746=CARTESIAN_POINT('',(-0.0099006579232147,0.0328108891324553,0.091));
#41747=CARTESIAN_POINT('',(-0.0175,0.0303108891324553,0.091));
#41748=CARTESIAN_POINT('',(-0.0099006579232147,0.0278108891324554,0.091));
#41749=CARTESIAN_POINT('',(-0.0099006579232147,0.0278108891324554,0.0142731879764631));
#41750=CARTESIAN_POINT('',(-0.0175,0.0303108891324553,0.091));
#41751=CARTESIAN_POINT('',(-0.0115,0.0303108891324553,0.091));
#41752=CARTESIAN_POINT('',(-0.01,0.0303108891324553,0.091));
#41753=CARTESIAN_POINT('',(-0.0175,0.0303108891324553,0.091));
#41754=CARTESIAN_POINT('',(-0.0274,0.0303108891324553,0.091));
#41755=CARTESIAN_POINT('',(-0.0115,0.0328108891324553,0.091));
#41756=CARTESIAN_POINT('',(-0.0115,0.0328108891324553,0.091));
#41757=CARTESIAN_POINT('',(-0.0115,0.0303108891324553,0.091));
#41758=CARTESIAN_POINT('',(-0.0115,0.0278108891324554,0.091));
#41759=CARTESIAN_POINT('',(-0.0115,0.0278108891324554,0.091));
#41760=CARTESIAN_POINT('',(-0.0115,0.0278108891324554,0.0142731879764631));
#41761=CARTESIAN_POINT('',(-0.0115,0.0278108891324554,0.0142731879764631));
#41762=CARTESIAN_POINT('',(-0.0115,0.0328108891324553,0.0142731879764631));
#41763=CARTESIAN_POINT('',(-0.0115,0.0328108891324553,0.0142731879764631));
#41764=CARTESIAN_POINT('',(-0.0115,0.0303108891324553,0.0142731879764631));
#41765=CARTESIAN_POINT('',(-0.0175,0.0303108891324553,0.021));
#41766=CARTESIAN_POINT('',(-0.00879583654340205,0.0308108891324553,0.021));
#41767=CARTESIAN_POINT('',(-0.00879583654340205,0.0298108891324554,0.021));
#41768=CARTESIAN_POINT('',(-0.0175,0.0303108891324553,0.021));
#41769=CARTESIAN_POINT('',(-0.0175,0.0303108891324553,0.021));
#41770=CARTESIAN_POINT('',(-0.0115,0.0303108891324553,0.021));
#41771=CARTESIAN_POINT('',(-0.0115,0.0303108891324553,0.021));
#41772=CARTESIAN_POINT('',(-0.0115,0.0303108891324553,0.021));
#41773=CARTESIAN_POINT('',(-0.0175,0.0303108891324553,0.091));
#41774=CARTESIAN_POINT('',(-0.0175,0.0303108891324553,0.014));
#41775=CARTESIAN_POINT('',(-0.00953134086570699,0.0310183293076278,0.026));
#41776=CARTESIAN_POINT('',(-0.00951275551339847,0.0308089825068169,0.0261464579794882));
#41777=CARTESIAN_POINT('',(-0.00948724312072826,0.0303094965600865,0.0263585979226248));
#41778=CARTESIAN_POINT('',(-0.00951275836916453,0.0298127635905308,0.0261464354752214));
#41779=CARTESIAN_POINT('',(-0.00953134086570699,0.029603448957283,0.026));
#41780=CARTESIAN_POINT('',(-0.0115,0.0303108891324553,0.0142731879764631));
#41781=CARTESIAN_POINT('',(-0.0115,0.0303108891324553,0.031));
#41782=CARTESIAN_POINT('',(-0.0115,0.0303108891324553,0.029));
#41783=CARTESIAN_POINT('',(-0.0105,0.0303108891324553,0.029));
#41784=CARTESIAN_POINT('',(-0.0115,0.0303108891324553,0.029));
#41785=CARTESIAN_POINT('',(-0.0115,0.0303108891324553,0.031));
#41786=CARTESIAN_POINT('',(-0.0115,0.0303108891324553,0.026));
#41787=CARTESIAN_POINT('',(-0.0115,0.0303108891324553,0.026));
#41788=CARTESIAN_POINT('',(-0.00879583654340205,0.0308108891324553,0.026));
#41789=CARTESIAN_POINT('',(-0.00879583654340205,0.0298108891324554,0.026));
#45463=MECHANICAL_DESIGN_GEOMETRIC_PRESENTATION_REPRESENTATION('',(#13552),#45464);
#45464=(
GEOMETRIC_REPRESENTATION_CONTEXT(3)
GLOBAL_UNCERTAINTY_ASSIGNED_CONTEXT((#45492))
GLOBAL_UNIT_ASSIGNED_CONTEXT((#45522,#45521,#45520))
REPRESENTATION_CONTEXT('MAS-690','TOP_LEVEL_ASSEMBLY_PART')
);
#45488=(
GEOMETRIC_REPRESENTATION_CONTEXT(3)
GLOBAL_UNCERTAINTY_ASSIGNED_CONTEXT((#45516))
GLOBAL_UNIT_ASSIGNED_CONTEXT((#45522,#45521,#45520))
REPRESENTATION_CONTEXT('refill_port','COMPONENT_PART')
);
#45492=UNCERTAINTY_MEASURE_WITH_UNIT(LENGTH_MEASURE(1.E-8),#45522,
'DISTANCE_ACCURACY_VALUE','Maximum Tolerance applied to model');
#45516=UNCERTAINTY_MEASURE_WITH_UNIT(LENGTH_MEASURE(2.E-5),#45522,
'DISTANCE_ACCURACY_VALUE','Maximum Tolerance applied to model');
#45520=(
NAMED_UNIT(*)
SI_UNIT($,.STERADIAN.)
SOLID_ANGLE_UNIT()
);
#45521=(
NAMED_UNIT(*)
PLANE_ANGLE_UNIT()
SI_UNIT($,.RADIAN.)
);
#45522=(
LENGTH_UNIT()
NAMED_UNIT(*)
SI_UNIT($,.METRE.)
);
#45577=PRODUCT_DEFINITION_SHAPE('','',#45609);
#45609=PRODUCT_DEFINITION('','',#45665,#45637);
#45637=PRODUCT_DEFINITION_CONTEXT('',#45782,'design');
#45665=PRODUCT_DEFINITION_FORMATION_WITH_SPECIFIED_SOURCE('','',#45721,
 .NOT_KNOWN.);
#45721=PRODUCT('refill_port','refill_port','refill_port',(#45777));
#45777=PRODUCT_CONTEXT('',#45782,'mechanical');
#45782=APPLICATION_CONTEXT('managed model based 3d engineering');
ENDSEC;
END-ISO-10303-21;
